ISO-10303-21;
HEADER;
/* Generated by software containing ST-Developer
 * from STEP Tools, Inc. (www.steptools.com) 
 */

FILE_DESCRIPTION(
/* description */ (''),
/* implementation_level */ '2;1');

FILE_NAME(
/* name */ '10_Compressor_Locknut_12pt_M7x1_LH.step',
/* time_stamp */ '2026-10-25T01:10:36-07:00',
/* author */ (''),
/* organization */ (''),
/* preprocessor_version */ 'ST-DEVELOPER v20.2',
/* originating_system */ 'Autodesk Translation Framework v15.15.0.0',
/* authorisation */ '');

FILE_SCHEMA (('AUTOMOTIVE_DESIGN { 1 0 10303 214 3 1 1 }'));
ENDSEC;

DATA;
#10=MECHANICAL_DESIGN_GEOMETRIC_PRESENTATION_REPRESENTATION('',(#1302),#60365);
#74=SHAPE_REPRESENTATION_RELATIONSHIP('SRR','None',#60414,#84);
#84=ADVANCED_BREP_SHAPE_REPRESENTATION('',(#94),#60362);
#94=MANIFOLD_SOLID_BREP('Body1',#18304);
#159=B_SPLINE_SURFACE_WITH_KNOTS('',3,3,((#57414,#57415,#57416,#57417),
(#57418,#57419,#57420,#57421),(#57422,#57423,#57424,#57425),(#57426,#57427,
#57428,#57429)),.UNSPECIFIED.,.F.,.F.,.F.,(4,4),(4,4),(0.,1.),(0.0769218004431789,
0.23169515901548),.UNSPECIFIED.);
#160=B_SPLINE_SURFACE_WITH_KNOTS('',3,3,((#57480,#57481,#57482,#57483),
(#57484,#57485,#57486,#57487),(#57488,#57489,#57490,#57491),(#57492,#57493,
#57494,#57495)),.UNSPECIFIED.,.F.,.F.,.F.,(4,4),(4,4),(0.,1.),(0.0769218004431759,
0.23169515901548),.UNSPECIFIED.);
#161=B_SPLINE_SURFACE_WITH_KNOTS('',3,3,((#57546,#57547,#57548,#57549),
(#57550,#57551,#57552,#57553),(#57554,#57555,#57556,#57557),(#57558,#57559,
#57560,#57561)),.UNSPECIFIED.,.F.,.F.,.F.,(4,4),(4,4),(0.,1.),(0.0769218004431517,
0.231695159015479),.UNSPECIFIED.);
#162=B_SPLINE_SURFACE_WITH_KNOTS('',3,3,((#57698,#57699,#57700,#57701),
(#57702,#57703,#57704,#57705),(#57706,#57707,#57708,#57709),(#57710,#57711,
#57712,#57713)),.UNSPECIFIED.,.F.,.F.,.F.,(4,4),(4,4),(0.,1.),(0.0769218004431787,
0.23169515901548),.UNSPECIFIED.);
#163=B_SPLINE_SURFACE_WITH_KNOTS('',3,3,((#57733,#57734,#57735,#57736),
(#57737,#57738,#57739,#57740),(#57741,#57742,#57743,#57744),(#57745,#57746,
#57747,#57748)),.UNSPECIFIED.,.F.,.F.,.F.,(4,4),(4,4),(0.,1.),(0.126990834822138,
0.281764193765889),.UNSPECIFIED.);
#164=B_SPLINE_SURFACE_WITH_KNOTS('',3,3,((#57798,#57799,#57800,#57801),
(#57802,#57803,#57804,#57805),(#57806,#57807,#57808,#57809),(#57810,#57811,
#57812,#57813)),.UNSPECIFIED.,.F.,.F.,.F.,(4,4),(4,4),(0.,1.),(0.0769218004431756,
0.231695159015479),.UNSPECIFIED.);
#165=B_SPLINE_SURFACE_WITH_KNOTS('',3,3,((#57828,#57829,#57830,#57831),
(#57832,#57833,#57834,#57835),(#57836,#57837,#57838,#57839),(#57840,#57841,
#57842,#57843)),.UNSPECIFIED.,.F.,.F.,.F.,(4,4),(4,4),(0.,1.),(0.126990834822142,
0.281764193765892),.UNSPECIFIED.);
#166=B_SPLINE_SURFACE_WITH_KNOTS('',3,3,((#57893,#57894,#57895,#57896),
(#57897,#57898,#57899,#57900),(#57901,#57902,#57903,#57904),(#57905,#57906,
#57907,#57908)),.UNSPECIFIED.,.F.,.F.,.F.,(4,4),(4,4),(0.,1.),(0.076921800443152,
0.231695159015479),.UNSPECIFIED.);
#167=B_SPLINE_SURFACE_WITH_KNOTS('',3,3,((#57954,#57955,#57956,#57957),
(#57958,#57959,#57960,#57961),(#57962,#57963,#57964,#57965),(#57966,#57967,
#57968,#57969)),.UNSPECIFIED.,.F.,.F.,.F.,(4,4),(4,4),(0.,1.),(0.0769218008186939,
0.221927025906161),.UNSPECIFIED.);
#168=B_SPLINE_SURFACE_WITH_KNOTS('',3,3,((#57980,#57981,#57982,#57983),
(#57984,#57985,#57986,#57987),(#57988,#57989,#57990,#57991),(#57992,#57993,
#57994,#57995)),.UNSPECIFIED.,.F.,.F.,.F.,(4,4),(4,4),(0.,1.),(0.12699083482214,
0.281764193752995),.UNSPECIFIED.);
#169=B_SPLINE_SURFACE_WITH_KNOTS('',3,3,((#58040,#58041,#58042,#58043),
(#58044,#58045,#58046,#58047),(#58048,#58049,#58050,#58051),(#58052,#58053,
#58054,#58055)),.UNSPECIFIED.,.F.,.F.,.F.,(4,4),(4,4),(0.,1.),(0.0769218004431788,
0.23169515901548),.UNSPECIFIED.);
#170=B_SPLINE_SURFACE_WITH_KNOTS('',3,3,((#58070,#58071,#58072,#58073),
(#58074,#58075,#58076,#58077),(#58078,#58079,#58080,#58081),(#58082,#58083,
#58084,#58085)),.UNSPECIFIED.,.F.,.F.,.F.,(4,4),(4,4),(0.,1.),(0.126990834822138,
0.281764193765889),.UNSPECIFIED.);
#171=B_SPLINE_SURFACE_WITH_KNOTS('',3,3,((#58135,#58136,#58137,#58138),
(#58139,#58140,#58141,#58142),(#58143,#58144,#58145,#58146),(#58147,#58148,
#58149,#58150)),.UNSPECIFIED.,.F.,.F.,.F.,(4,4),(4,4),(0.,1.),(0.0769218004431755,
0.231695159015479),.UNSPECIFIED.);
#172=B_SPLINE_SURFACE_WITH_KNOTS('',3,3,((#58165,#58166,#58167,#58168),
(#58169,#58170,#58171,#58172),(#58173,#58174,#58175,#58176),(#58177,#58178,
#58179,#58180)),.UNSPECIFIED.,.F.,.F.,.F.,(4,4),(4,4),(0.,1.),(0.126990834822142,
0.281764193765893),.UNSPECIFIED.);
#173=B_SPLINE_SURFACE_WITH_KNOTS('',3,3,((#58230,#58231,#58232,#58233),
(#58234,#58235,#58236,#58237),(#58238,#58239,#58240,#58241),(#58242,#58243,
#58244,#58245)),.UNSPECIFIED.,.F.,.F.,.F.,(4,4),(4,4),(0.,1.),(0.0769218004431519,
0.23169515901548),.UNSPECIFIED.);
#174=B_SPLINE_SURFACE_WITH_KNOTS('',3,3,((#58260,#58261,#58262,#58263),
(#58264,#58265,#58266,#58267),(#58268,#58269,#58270,#58271),(#58272,#58273,
#58274,#58275)),.UNSPECIFIED.,.F.,.F.,.F.,(4,4),(4,4),(0.,1.),(0.126990834822139,
0.28176419376589),.UNSPECIFIED.);
#175=B_SPLINE_SURFACE_WITH_KNOTS('',3,3,((#58289,#58290,#58291,#58292),
(#58293,#58294,#58295,#58296),(#58297,#58298,#58299,#58300),(#58301,#58302,
#58303,#58304)),.UNSPECIFIED.,.F.,.F.,.F.,(4,4),(4,4),(0.380102179090416,
1.),(0.231695159015479,0.246948509226624),.UNSPECIFIED.);
#176=B_SPLINE_SURFACE_WITH_KNOTS('',3,3,((#58322,#58323,#58324,#58325),
(#58326,#58327,#58328,#58329),(#58330,#58331,#58332,#58333),(#58334,#58335,
#58336,#58337)),.UNSPECIFIED.,.F.,.F.,.F.,(4,4),(4,4),(0.380102179090417,
1.),(0.231695159015479,0.246948509226624),.UNSPECIFIED.);
#177=B_SPLINE_SURFACE_WITH_KNOTS('',3,3,((#58355,#58356,#58357,#58358),
(#58359,#58360,#58361,#58362),(#58363,#58364,#58365,#58366),(#58367,#58368,
#58369,#58370)),.UNSPECIFIED.,.F.,.F.,.F.,(4,4),(4,4),(0.380102179090425,
1.),(0.23169515901548,0.246948509226623),.UNSPECIFIED.);
#178=B_SPLINE_SURFACE_WITH_KNOTS('',3,3,((#58388,#58389,#58390,#58391),
(#58392,#58393,#58394,#58395),(#58396,#58397,#58398,#58399),(#58400,#58401,
#58402,#58403)),.UNSPECIFIED.,.F.,.F.,.F.,(4,4),(4,4),(0.380102179090409,
1.),(0.23169515901548,0.246948509226625),.UNSPECIFIED.);
#179=B_SPLINE_SURFACE_WITH_KNOTS('',3,3,((#58421,#58422,#58423,#58424),
(#58425,#58426,#58427,#58428),(#58429,#58430,#58431,#58432),(#58433,#58434,
#58435,#58436)),.UNSPECIFIED.,.F.,.F.,.F.,(4,4),(4,4),(0.380102179090415,
1.),(0.231695159015479,0.246948509226624),.UNSPECIFIED.);
#180=B_SPLINE_SURFACE_WITH_KNOTS('',3,3,((#58454,#58455,#58456,#58457),
(#58458,#58459,#58460,#58461),(#58462,#58463,#58464,#58465),(#58466,#58467,
#58468,#58469)),.UNSPECIFIED.,.F.,.F.,.F.,(4,4),(4,4),(0.380102179090434,
1.),(0.23169515901548,0.246948509226623),.UNSPECIFIED.);
#181=B_SPLINE_SURFACE_WITH_KNOTS('',3,3,((#58487,#58488,#58489,#58490),
(#58491,#58492,#58493,#58494),(#58495,#58496,#58497,#58498),(#58499,#58500,
#58501,#58502)),.UNSPECIFIED.,.F.,.F.,.F.,(4,4),(4,4),(0.,1.),(0.12699083482214,
0.281764193765889),.UNSPECIFIED.);
#182=B_SPLINE_SURFACE_WITH_KNOTS('',3,3,((#58516,#58517,#58518,#58519),
(#58520,#58521,#58522,#58523),(#58524,#58525,#58526,#58527),(#58528,#58529,
#58530,#58531)),.UNSPECIFIED.,.F.,.F.,.F.,(4,4),(4,4),(0.380102179091578,
1.),(0.23169515901548,0.246948509226623),.UNSPECIFIED.);
#183=B_SPLINE_SURFACE_WITH_KNOTS('',3,3,((#58549,#58550,#58551,#58552),
(#58553,#58554,#58555,#58556),(#58557,#58558,#58559,#58560),(#58561,#58562,
#58563,#58564)),.UNSPECIFIED.,.F.,.F.,.F.,(4,4),(4,4),(0.,1.),(0.12699083482214,
0.28176419376589),.UNSPECIFIED.);
#184=B_SPLINE_SURFACE_WITH_KNOTS('',3,3,((#58578,#58579,#58580,#58581),
(#58582,#58583,#58584,#58585),(#58586,#58587,#58588,#58589),(#58590,#58591,
#58592,#58593)),.UNSPECIFIED.,.F.,.F.,.F.,(4,4),(4,4),(0.380102179091699,
1.),(0.23169515901548,0.246948509226624),.UNSPECIFIED.);
#185=B_SPLINE_SURFACE_WITH_KNOTS('',3,3,((#58611,#58612,#58613,#58614),
(#58615,#58616,#58617,#58618),(#58619,#58620,#58621,#58622),(#58623,#58624,
#58625,#58626)),.UNSPECIFIED.,.F.,.F.,.F.,(4,4),(4,4),(0.,1.),(0.12699083482214,
0.28176419376589),.UNSPECIFIED.);
#186=B_SPLINE_SURFACE_WITH_KNOTS('',3,3,((#58640,#58641,#58642,#58643),
(#58644,#58645,#58646,#58647),(#58648,#58649,#58650,#58651),(#58652,#58653,
#58654,#58655)),.UNSPECIFIED.,.F.,.F.,.F.,(4,4),(4,4),(0.380102179091715,
1.),(0.231695159015479,0.246948509226624),.UNSPECIFIED.);
#187=B_SPLINE_SURFACE_WITH_KNOTS('',3,3,((#58668,#58669,#58670,#58671),
(#58672,#58673,#58674,#58675),(#58676,#58677,#58678,#58679),(#58680,#58681,
#58682,#58683)),.UNSPECIFIED.,.F.,.F.,.F.,(4,4),(4,4),(0.,1.),(0.136758967931396,
0.281764193742676),.UNSPECIFIED.);
#188=B_SPLINE_SURFACE_WITH_KNOTS('',3,3,((#58688,#58689,#58690,#58691),
(#58692,#58693,#58694,#58695),(#58696,#58697,#58698,#58699),(#58700,#58701,
#58702,#58703)),.UNSPECIFIED.,.F.,.F.,.F.,(4,4),(4,4),(0.380102179091685,
1.),(0.111737484610932,0.12699083482214),.UNSPECIFIED.);
#189=B_SPLINE_SURFACE_WITH_KNOTS('',3,3,((#58713,#58714,#58715,#58716),
(#58717,#58718,#58719,#58720),(#58721,#58722,#58723,#58724),(#58725,#58726,
#58727,#58728)),.UNSPECIFIED.,.F.,.F.,.F.,(4,4),(4,4),(0.380102179091672,
1.),(0.111737484610932,0.12699083482214),.UNSPECIFIED.);
#190=B_SPLINE_SURFACE_WITH_KNOTS('',3,3,((#58738,#58739,#58740,#58741),
(#58742,#58743,#58744,#58745),(#58746,#58747,#58748,#58749),(#58750,#58751,
#58752,#58753)),.UNSPECIFIED.,.F.,.F.,.F.,(4,4),(4,4),(0.380102179091554,
1.),(0.111737484610934,0.12699083482214),.UNSPECIFIED.);
#191=B_SPLINE_SURFACE_WITH_KNOTS('',3,3,((#58763,#58764,#58765,#58766),
(#58767,#58768,#58769,#58770),(#58771,#58772,#58773,#58774),(#58775,#58776,
#58777,#58778)),.UNSPECIFIED.,.F.,.F.,.F.,(4,4),(4,4),(0.38010217909041,
1.),(0.111737484610934,0.12699083482214),.UNSPECIFIED.);
#192=B_SPLINE_SURFACE_WITH_KNOTS('',3,3,((#58783,#58784,#58785,#58786),
(#58787,#58788,#58789,#58790),(#58791,#58792,#58793,#58794),(#58795,#58796,
#58797,#58798)),.UNSPECIFIED.,.F.,.F.,.F.,(4,4),(4,4),(0.380102179090392,
1.),(0.11173748461093,0.126990834822138),.UNSPECIFIED.);
#193=B_SPLINE_SURFACE_WITH_KNOTS('',3,3,((#58808,#58809,#58810,#58811),
(#58812,#58813,#58814,#58815),(#58816,#58817,#58818,#58819),(#58820,#58821,
#58822,#58823)),.UNSPECIFIED.,.F.,.F.,.F.,(4,4),(4,4),(0.380102179090381,
1.),(0.111737484610934,0.126990834822142),.UNSPECIFIED.);
#194=B_SPLINE_SURFACE_WITH_KNOTS('',3,3,((#58833,#58834,#58835,#58836),
(#58837,#58838,#58839,#58840),(#58841,#58842,#58843,#58844),(#58845,#58846,
#58847,#58848)),.UNSPECIFIED.,.F.,.F.,.F.,(4,4),(4,4),(0.380102179090396,
1.),(0.111737484610932,0.126990834822139),.UNSPECIFIED.);
#195=B_SPLINE_SURFACE_WITH_KNOTS('',3,3,((#58858,#58859,#58860,#58861),
(#58862,#58863,#58864,#58865),(#58866,#58867,#58868,#58869),(#58870,#58871,
#58872,#58873)),.UNSPECIFIED.,.F.,.F.,.F.,(4,4),(4,4),(0.380102179090391,
1.),(0.11173748461093,0.126990834822138),.UNSPECIFIED.);
#196=B_SPLINE_SURFACE_WITH_KNOTS('',3,3,((#58883,#58884,#58885,#58886),
(#58887,#58888,#58889,#58890),(#58891,#58892,#58893,#58894),(#58895,#58896,
#58897,#58898)),.UNSPECIFIED.,.F.,.F.,.F.,(4,4),(4,4),(0.380102179090391,
1.),(0.111737484610934,0.126990834822142),.UNSPECIFIED.);
#243=FACE_BOUND('',#3069,.T.);
#244=FACE_BOUND('',#3090,.T.);
#245=FACE_BOUND('',#3095,.T.);
#624=PLANE('',#19369);
#625=PLANE('',#19370);
#626=PLANE('',#19371);
#627=PLANE('',#19372);
#628=PLANE('',#19373);
#629=PLANE('',#19374);
#630=PLANE('',#19375);
#631=PLANE('',#19376);
#632=PLANE('',#19379);
#633=PLANE('',#19380);
#634=PLANE('',#19381);
#635=PLANE('',#19382);
#636=PLANE('',#19383);
#637=PLANE('',#19384);
#638=PLANE('',#19385);
#639=PLANE('',#19386);
#640=PLANE('',#19387);
#641=PLANE('',#19388);
#642=PLANE('',#19389);
#643=PLANE('',#19390);
#644=PLANE('',#19391);
#645=PLANE('',#19392);
#646=PLANE('',#19393);
#647=PLANE('',#19394);
#648=PLANE('',#19395);
#649=PLANE('',#19396);
#650=PLANE('',#19397);
#651=PLANE('',#19398);
#652=PLANE('',#19399);
#653=PLANE('',#19422);
#654=PLANE('',#19423);
#655=PLANE('',#19424);
#656=PLANE('',#19425);
#657=PLANE('',#19426);
#658=PLANE('',#19427);
#659=PLANE('',#19428);
#660=PLANE('',#19429);
#661=PLANE('',#19431);
#662=PLANE('',#19439);
#955=CONICAL_SURFACE('',#19377,5.3,0.862170054667227);
#956=CONICAL_SURFACE('',#19409,5.3,0.862170054667227);
#957=CONICAL_SURFACE('',#19410,5.3,0.862170054667227);
#958=CONICAL_SURFACE('',#19411,5.3,0.862170054667227);
#959=CONICAL_SURFACE('',#19412,5.3,0.862170054667227);
#960=CONICAL_SURFACE('',#19413,5.3,0.862170054667227);
#961=CONICAL_SURFACE('',#19414,5.3,0.862170054667227);
#962=CONICAL_SURFACE('',#19415,5.3,0.862170054667227);
#963=CONICAL_SURFACE('',#19416,5.3,0.862170054667227);
#964=CONICAL_SURFACE('',#19417,3.8,0.785398163397448);
#965=CONICAL_SURFACE('',#19419,3.8,0.785398163397448);
#966=CONICAL_SURFACE('',#19433,6.35,0.785398163397449);
#967=CONICAL_SURFACE('',#19437,6.25,1.19028994968253);
#1056=(
BOUNDED_CURVE()
B_SPLINE_CURVE(2,(#57584,#57585,#57586),.UNSPECIFIED.,.F.,.F.)
B_SPLINE_CURVE_WITH_KNOTS((3,3),(0.111972083330786,0.162414552121297),
 .UNSPECIFIED.)
CURVE()
GEOMETRIC_REPRESENTATION_ITEM()
RATIONAL_B_SPLINE_CURVE((1.01528943481759,1.01635902992211,1.01528943481759))
REPRESENTATION_ITEM('')
);
#1057=(
BOUNDED_CURVE()
B_SPLINE_CURVE(2,(#57594,#57595,#57596),.UNSPECIFIED.,.F.,.F.)
B_SPLINE_CURVE_WITH_KNOTS((3,3),(0.09935665845201,0.231695159015479),
 .UNSPECIFIED.)
CURVE()
GEOMETRIC_REPRESENTATION_ITEM()
RATIONAL_B_SPLINE_CURVE((1.02178152598816,1.03072985007612,1.02487304850091))
REPRESENTATION_ITEM('')
);
#1058=(
BOUNDED_CURVE()
B_SPLINE_CURVE(2,(#57598,#57599,#57600),.UNSPECIFIED.,.F.,.F.)
B_SPLINE_CURVE_WITH_KNOTS((3,3),(0.154087551415272,0.195687290922671),
 .UNSPECIFIED.)
CURVE()
GEOMETRIC_REPRESENTATION_ITEM()
RATIONAL_B_SPLINE_CURVE((1.01731872616523,1.01669262938109,1.01446617353995))
REPRESENTATION_ITEM('')
);
#1059=(
BOUNDED_CURVE()
B_SPLINE_CURVE(2,(#57613,#57614,#57615),.UNSPECIFIED.,.F.,.F.)
B_SPLINE_CURVE_WITH_KNOTS((3,3),(0.126990834822139,0.259329335387418),
 .UNSPECIFIED.)
CURVE()
GEOMETRIC_REPRESENTATION_ITEM()
RATIONAL_B_SPLINE_CURVE((1.02487304850069,1.03072985007626,1.02178152598826))
REPRESENTATION_ITEM('')
);
#1060=(
BOUNDED_CURVE()
B_SPLINE_CURVE(2,(#57617,#57618,#57619),.UNSPECIFIED.,.F.,.F.)
B_SPLINE_CURVE_WITH_KNOTS((3,3),(0.09935665845201,0.23169515901548),
 .UNSPECIFIED.)
CURVE()
GEOMETRIC_REPRESENTATION_ITEM()
RATIONAL_B_SPLINE_CURVE((1.02178152598816,1.03072985007612,1.02487304850091))
REPRESENTATION_ITEM('')
);
#1061=(
BOUNDED_CURVE()
B_SPLINE_CURVE(2,(#57621,#57622,#57623),.UNSPECIFIED.,.F.,.F.)
B_SPLINE_CURVE_WITH_KNOTS((3,3),(0.111972083330787,0.162414552121298),
 .UNSPECIFIED.)
CURVE()
GEOMETRIC_REPRESENTATION_ITEM()
RATIONAL_B_SPLINE_CURVE((1.01528943481758,1.01635902992211,1.01528943481758))
REPRESENTATION_ITEM('')
);
#1062=(
BOUNDED_CURVE()
B_SPLINE_CURVE(2,(#57625,#57626,#57627),.UNSPECIFIED.,.F.,.F.)
B_SPLINE_CURVE_WITH_KNOTS((3,3),(0.126990834822138,0.259329335387416),
 .UNSPECIFIED.)
CURVE()
GEOMETRIC_REPRESENTATION_ITEM()
RATIONAL_B_SPLINE_CURVE((1.02487304850069,1.03072985007626,1.02178152598826))
REPRESENTATION_ITEM('')
);
#1063=(
BOUNDED_CURVE()
B_SPLINE_CURVE(2,(#57629,#57630,#57631),.UNSPECIFIED.,.F.,.F.)
B_SPLINE_CURVE_WITH_KNOTS((3,3),(0.0799382874584893,0.121538026965825),
 .UNSPECIFIED.)
CURVE()
GEOMETRIC_REPRESENTATION_ITEM()
RATIONAL_B_SPLINE_CURVE((1.01446617353996,1.0166926293811,1.01731872616524))
REPRESENTATION_ITEM('')
);
#1302=STYLED_ITEM('',(#60534),#94);
#1991=FACE_OUTER_BOUND('',#3001,.T.);
#1992=FACE_OUTER_BOUND('',#3002,.T.);
#1993=FACE_OUTER_BOUND('',#3003,.T.);
#1994=FACE_OUTER_BOUND('',#3004,.T.);
#1995=FACE_OUTER_BOUND('',#3005,.T.);
#1996=FACE_OUTER_BOUND('',#3006,.T.);
#1997=FACE_OUTER_BOUND('',#3007,.T.);
#1998=FACE_OUTER_BOUND('',#3008,.T.);
#1999=FACE_OUTER_BOUND('',#3009,.T.);
#2000=FACE_OUTER_BOUND('',#3010,.T.);
#2001=FACE_OUTER_BOUND('',#3011,.T.);
#2002=FACE_OUTER_BOUND('',#3012,.T.);
#2003=FACE_OUTER_BOUND('',#3013,.T.);
#2004=FACE_OUTER_BOUND('',#3014,.T.);
#2005=FACE_OUTER_BOUND('',#3015,.T.);
#2006=FACE_OUTER_BOUND('',#3016,.T.);
#2007=FACE_OUTER_BOUND('',#3017,.T.);
#2008=FACE_OUTER_BOUND('',#3018,.T.);
#2009=FACE_OUTER_BOUND('',#3019,.T.);
#2010=FACE_OUTER_BOUND('',#3020,.T.);
#2011=FACE_OUTER_BOUND('',#3021,.T.);
#2012=FACE_OUTER_BOUND('',#3022,.T.);
#2013=FACE_OUTER_BOUND('',#3023,.T.);
#2014=FACE_OUTER_BOUND('',#3024,.T.);
#2015=FACE_OUTER_BOUND('',#3025,.T.);
#2016=FACE_OUTER_BOUND('',#3026,.T.);
#2017=FACE_OUTER_BOUND('',#3027,.T.);
#2018=FACE_OUTER_BOUND('',#3028,.T.);
#2019=FACE_OUTER_BOUND('',#3029,.T.);
#2020=FACE_OUTER_BOUND('',#3030,.T.);
#2021=FACE_OUTER_BOUND('',#3031,.T.);
#2022=FACE_OUTER_BOUND('',#3032,.T.);
#2023=FACE_OUTER_BOUND('',#3033,.T.);
#2024=FACE_OUTER_BOUND('',#3034,.T.);
#2025=FACE_OUTER_BOUND('',#3035,.T.);
#2026=FACE_OUTER_BOUND('',#3036,.T.);
#2027=FACE_OUTER_BOUND('',#3037,.T.);
#2028=FACE_OUTER_BOUND('',#3038,.T.);
#2029=FACE_OUTER_BOUND('',#3039,.T.);
#2030=FACE_OUTER_BOUND('',#3040,.T.);
#2031=FACE_OUTER_BOUND('',#3041,.T.);
#2032=FACE_OUTER_BOUND('',#3042,.T.);
#2033=FACE_OUTER_BOUND('',#3043,.T.);
#2034=FACE_OUTER_BOUND('',#3044,.T.);
#2035=FACE_OUTER_BOUND('',#3045,.T.);
#2036=FACE_OUTER_BOUND('',#3046,.T.);
#2037=FACE_OUTER_BOUND('',#3047,.T.);
#2038=FACE_OUTER_BOUND('',#3048,.T.);
#2039=FACE_OUTER_BOUND('',#3049,.T.);
#2040=FACE_OUTER_BOUND('',#3050,.T.);
#2041=FACE_OUTER_BOUND('',#3051,.T.);
#2042=FACE_OUTER_BOUND('',#3052,.T.);
#2043=FACE_OUTER_BOUND('',#3053,.T.);
#2044=FACE_OUTER_BOUND('',#3054,.T.);
#2045=FACE_OUTER_BOUND('',#3055,.T.);
#2046=FACE_OUTER_BOUND('',#3056,.T.);
#2047=FACE_OUTER_BOUND('',#3057,.T.);
#2048=FACE_OUTER_BOUND('',#3058,.T.);
#2049=FACE_OUTER_BOUND('',#3059,.T.);
#2050=FACE_OUTER_BOUND('',#3060,.T.);
#2051=FACE_OUTER_BOUND('',#3061,.T.);
#2052=FACE_OUTER_BOUND('',#3062,.T.);
#2053=FACE_OUTER_BOUND('',#3063,.T.);
#2054=FACE_OUTER_BOUND('',#3064,.T.);
#2055=FACE_OUTER_BOUND('',#3065,.T.);
#2056=FACE_OUTER_BOUND('',#3066,.T.);
#2057=FACE_OUTER_BOUND('',#3067,.T.);
#2058=FACE_OUTER_BOUND('',#3068,.T.);
#2059=FACE_OUTER_BOUND('',#3070,.T.);
#2060=FACE_OUTER_BOUND('',#3071,.T.);
#2061=FACE_OUTER_BOUND('',#3072,.T.);
#2062=FACE_OUTER_BOUND('',#3073,.T.);
#2063=FACE_OUTER_BOUND('',#3074,.T.);
#2064=FACE_OUTER_BOUND('',#3075,.T.);
#2065=FACE_OUTER_BOUND('',#3076,.T.);
#2066=FACE_OUTER_BOUND('',#3077,.T.);
#2067=FACE_OUTER_BOUND('',#3078,.T.);
#2068=FACE_OUTER_BOUND('',#3079,.T.);
#2069=FACE_OUTER_BOUND('',#3080,.T.);
#2070=FACE_OUTER_BOUND('',#3081,.T.);
#2071=FACE_OUTER_BOUND('',#3082,.T.);
#2072=FACE_OUTER_BOUND('',#3083,.T.);
#2073=FACE_OUTER_BOUND('',#3084,.T.);
#2074=FACE_OUTER_BOUND('',#3085,.T.);
#2075=FACE_OUTER_BOUND('',#3086,.T.);
#2076=FACE_OUTER_BOUND('',#3087,.T.);
#2077=FACE_OUTER_BOUND('',#3088,.T.);
#2078=FACE_OUTER_BOUND('',#3089,.T.);
#2079=FACE_OUTER_BOUND('',#3091,.T.);
#2080=FACE_OUTER_BOUND('',#3092,.T.);
#2081=FACE_OUTER_BOUND('',#3093,.T.);
#2082=FACE_OUTER_BOUND('',#3094,.T.);
#3001=EDGE_LOOP('',(#15659,#15660,#15661,#15662,#15663));
#3002=EDGE_LOOP('',(#15664,#15665,#15666,#15667));
#3003=EDGE_LOOP('',(#15668,#15669,#15670,#15671,#15672,#15673));
#3004=EDGE_LOOP('',(#15674,#15675,#15676,#15677,#15678));
#3005=EDGE_LOOP('',(#15679,#15680,#15681,#15682));
#3006=EDGE_LOOP('',(#15683,#15684,#15685,#15686,#15687,#15688));
#3007=EDGE_LOOP('',(#15689,#15690,#15691,#15692,#15693));
#3008=EDGE_LOOP('',(#15694,#15695,#15696,#15697));
#3009=EDGE_LOOP('',(#15698,#15699,#15700,#15701,#15702,#15703));
#3010=EDGE_LOOP('',(#15704,#15705,#15706,#15707));
#3011=EDGE_LOOP('',(#15708,#15709,#15710,#15711,#15712,#15713));
#3012=EDGE_LOOP('',(#15714,#15715,#15716,#15717,#15718,#15719,#15720,#15721,
#15722,#15723,#15724,#15725,#15726,#15727,#15728));
#3013=EDGE_LOOP('',(#15729,#15730,#15731,#15732));
#3014=EDGE_LOOP('',(#15733,#15734,#15735,#15736));
#3015=EDGE_LOOP('',(#15737,#15738,#15739,#15740,#15741));
#3016=EDGE_LOOP('',(#15742,#15743,#15744,#15745));
#3017=EDGE_LOOP('',(#15746,#15747,#15748,#15749,#15750,#15751));
#3018=EDGE_LOOP('',(#15752,#15753,#15754,#15755,#15756,#15757));
#3019=EDGE_LOOP('',(#15758,#15759,#15760,#15761,#15762));
#3020=EDGE_LOOP('',(#15763,#15764,#15765,#15766));
#3021=EDGE_LOOP('',(#15767,#15768,#15769,#15770,#15771,#15772));
#3022=EDGE_LOOP('',(#15773,#15774,#15775,#15776,#15777,#15778));
#3023=EDGE_LOOP('',(#15779,#15780,#15781,#15782,#15783));
#3024=EDGE_LOOP('',(#15784,#15785,#15786,#15787));
#3025=EDGE_LOOP('',(#15788,#15789,#15790,#15791,#15792,#15793));
#3026=EDGE_LOOP('',(#15794,#15795,#15796,#15797,#15798));
#3027=EDGE_LOOP('',(#15799,#15800,#15801,#15802));
#3028=EDGE_LOOP('',(#15803,#15804,#15805,#15806,#15807));
#3029=EDGE_LOOP('',(#15808,#15809,#15810,#15811,#15812,#15813));
#3030=EDGE_LOOP('',(#15814,#15815,#15816,#15817,#15818));
#3031=EDGE_LOOP('',(#15819,#15820,#15821,#15822));
#3032=EDGE_LOOP('',(#15823,#15824,#15825,#15826,#15827,#15828));
#3033=EDGE_LOOP('',(#15829,#15830,#15831,#15832,#15833,#15834));
#3034=EDGE_LOOP('',(#15835,#15836,#15837,#15838,#15839));
#3035=EDGE_LOOP('',(#15840,#15841,#15842,#15843));
#3036=EDGE_LOOP('',(#15844,#15845,#15846,#15847,#15848,#15849));
#3037=EDGE_LOOP('',(#15850,#15851,#15852,#15853,#15854,#15855));
#3038=EDGE_LOOP('',(#15856,#15857,#15858,#15859,#15860));
#3039=EDGE_LOOP('',(#15861,#15862,#15863,#15864));
#3040=EDGE_LOOP('',(#15865,#15866,#15867,#15868,#15869,#15870));
#3041=EDGE_LOOP('',(#15871,#15872,#15873,#15874,#15875,#15876));
#3042=EDGE_LOOP('',(#15877,#15878,#15879,#15880));
#3043=EDGE_LOOP('',(#15881,#15882,#15883,#15884));
#3044=EDGE_LOOP('',(#15885,#15886,#15887,#15888));
#3045=EDGE_LOOP('',(#15889,#15890,#15891,#15892));
#3046=EDGE_LOOP('',(#15893,#15894,#15895,#15896));
#3047=EDGE_LOOP('',(#15897,#15898,#15899,#15900));
#3048=EDGE_LOOP('',(#15901,#15902,#15903,#15904,#15905,#15906));
#3049=EDGE_LOOP('',(#15907,#15908,#15909,#15910));
#3050=EDGE_LOOP('',(#15911,#15912,#15913,#15914,#15915,#15916));
#3051=EDGE_LOOP('',(#15917,#15918,#15919,#15920));
#3052=EDGE_LOOP('',(#15921,#15922,#15923,#15924,#15925,#15926));
#3053=EDGE_LOOP('',(#15927,#15928,#15929,#15930));
#3054=EDGE_LOOP('',(#15931,#15932,#15933,#15934,#15935));
#3055=EDGE_LOOP('',(#15936,#15937,#15938,#15939));
#3056=EDGE_LOOP('',(#15940,#15941,#15942,#15943));
#3057=EDGE_LOOP('',(#15944,#15945,#15946,#15947));
#3058=EDGE_LOOP('',(#15948,#15949,#15950,#15951));
#3059=EDGE_LOOP('',(#15952,#15953,#15954,#15955));
#3060=EDGE_LOOP('',(#15956,#15957,#15958,#15959));
#3061=EDGE_LOOP('',(#15960,#15961,#15962,#15963));
#3062=EDGE_LOOP('',(#15964,#15965,#15966,#15967));
#3063=EDGE_LOOP('',(#15968,#15969,#15970,#15971));
#3064=EDGE_LOOP('',(#15972,#15973,#15974,#15975));
#3065=EDGE_LOOP('',(#15976,#15977,#15978,#15979));
#3066=EDGE_LOOP('',(#15980,#15981,#15982,#15983));
#3067=EDGE_LOOP('',(#15984,#15985,#15986,#15987));
#3068=EDGE_LOOP('',(#15988,#15989,#15990,#15991,#15992,#15993,#15994,#15995,
#15996,#15997,#15998,#15999,#16000,#16001,#16002,#16003,#16004,#16005,#16006,
#16007,#16008,#16009,#16010,#16011,#16012,#16013,#16014));
#3069=EDGE_LOOP('',(#16015));
#3070=EDGE_LOOP('',(#16016,#16017,#16018,#16019,#16020));
#3071=EDGE_LOOP('',(#16021,#16022,#16023,#16024,#16025));
#3072=EDGE_LOOP('',(#16026,#16027,#16028,#16029,#16030));
#3073=EDGE_LOOP('',(#16031,#16032,#16033,#16034,#16035));
#3074=EDGE_LOOP('',(#16036,#16037,#16038,#16039,#16040));
#3075=EDGE_LOOP('',(#16041,#16042,#16043,#16044,#16045));
#3076=EDGE_LOOP('',(#16046,#16047,#16048,#16049,#16050));
#3077=EDGE_LOOP('',(#16051,#16052,#16053,#16054,#16055));
#3078=EDGE_LOOP('',(#16056,#16057,#16058,#16059));
#3079=EDGE_LOOP('',(#16060,#16061,#16062,#16063));
#3080=EDGE_LOOP('',(#16064,#16065,#16066,#16067));
#3081=EDGE_LOOP('',(#16068,#16069,#16070,#16071));
#3082=EDGE_LOOP('',(#16072,#16073,#16074,#16075,#16076,#16077));
#3083=EDGE_LOOP('',(#16078,#16079,#16080,#16081));
#3084=EDGE_LOOP('',(#16082,#16083,#16084,#16085));
#3085=EDGE_LOOP('',(#16086,#16087,#16088,#16089));
#3086=EDGE_LOOP('',(#16090,#16091,#16092,#16093));
#3087=EDGE_LOOP('',(#16094,#16095,#16096,#16097));
#3088=EDGE_LOOP('',(#16098,#16099,#16100,#16101));
#3089=EDGE_LOOP('',(#16102));
#3090=EDGE_LOOP('',(#16103));
#3091=EDGE_LOOP('',(#16104,#16105,#16106,#16107));
#3092=EDGE_LOOP('',(#16108,#16109,#16110,#16111));
#3093=EDGE_LOOP('',(#16112,#16113,#16114,#16115));
#3094=EDGE_LOOP('',(#16116));
#3095=EDGE_LOOP('',(#16117,#16118,#16119,#16120,#16121,#16122,#16123,#16124,
#16125,#16126,#16127,#16128,#16129,#16130,#16131,#16132,#16133,#16134,#16135,
#16136,#16137,#16138,#16139,#16140,#16141,#16142,#16143,#16144,#16145,#16146,
#16147,#16148,#16149,#16150,#16151,#16152));
#3652=CIRCLE('',#19378,4.6);
#3653=CIRCLE('',#19400,4.6);
#3654=CIRCLE('',#19401,4.6);
#3655=CIRCLE('',#19402,4.6);
#3656=CIRCLE('',#19403,4.6);
#3657=CIRCLE('',#19404,4.6);
#3658=CIRCLE('',#19405,4.6);
#3659=CIRCLE('',#19406,4.6);
#3660=CIRCLE('',#19407,4.6);
#3661=CIRCLE('',#19408,3.95);
#3662=CIRCLE('',#19418,3.55);
#3663=CIRCLE('',#19420,3.95);
#3664=CIRCLE('',#19421,3.55);
#3665=CIRCLE('',#19432,6.2);
#3666=CIRCLE('',#19434,6.5);
#3667=CIRCLE('',#19436,6.5);
#3668=CIRCLE('',#19438,6.);
#4339=B_SPLINE_CURVE_WITH_KNOTS('',3,(#57386,#57387,#57388,#57389,#57390,
#57391,#57392),.UNSPECIFIED.,.F.,.F.,(4,3,4),(-0.0308504286108349,-0.027608334705132,
0.),.UNSPECIFIED.);
#4340=B_SPLINE_CURVE_WITH_KNOTS('',3,(#57399,#57400,#57401,#57402,#57403,
#57404),.UNSPECIFIED.,.F.,.F.,(4,2,4),(-0.0558053859643163,-0.0275791003961777,
-0.0249547869966958),.UNSPECIFIED.);
#4341=B_SPLINE_CURVE_WITH_KNOTS('',3,(#57407,#57408,#57409,#57410),
 .UNSPECIFIED.,.F.,.F.,(4,4),(-0.221927025840791,-0.0865063411776193),
 .UNSPECIFIED.);
#4342=B_SPLINE_CURVE_WITH_KNOTS('',3,(#57431,#57432,#57433,#57434),
 .UNSPECIFIED.,.F.,.F.,(4,4),(-0.0621213240389596,-0.0358629876218588),
 .UNSPECIFIED.);
#4343=B_SPLINE_CURVE_WITH_KNOTS('',3,(#57436,#57437,#57438,#57439),
 .UNSPECIFIED.,.F.,.F.,(4,4),(0.0934461854545239,0.23169515901548),
 .UNSPECIFIED.);
#4344=B_SPLINE_CURVE_WITH_KNOTS('',3,(#57441,#57442,#57443,#57444),
 .UNSPECIFIED.,.F.,.F.,(4,4),(-1.,-0.380102179092201),.UNSPECIFIED.);
#4345=B_SPLINE_CURVE_WITH_KNOTS('',3,(#57445,#57446,#57447,#57448),
 .UNSPECIFIED.,.F.,.F.,(4,4),(0.03639808094533,0.0611452087600889),
 .UNSPECIFIED.);
#4346=B_SPLINE_CURVE_WITH_KNOTS('',3,(#57452,#57453,#57454,#57455,#57456,
#57457,#57458),.UNSPECIFIED.,.F.,.F.,(4,3,4),(-0.0308504286108392,-0.0276083347051348,
0.),.UNSPECIFIED.);
#4347=B_SPLINE_CURVE_WITH_KNOTS('',3,(#57465,#57466,#57467,#57468,#57469,
#57470),.UNSPECIFIED.,.F.,.F.,(4,2,4),(-0.0558053859644324,-0.0275791003962552,
-0.0249547869967625),.UNSPECIFIED.);
#4348=B_SPLINE_CURVE_WITH_KNOTS('',3,(#57473,#57474,#57475,#57476),
 .UNSPECIFIED.,.F.,.F.,(4,4),(-0.221927025840791,-0.0865063411776191),
 .UNSPECIFIED.);
#4349=B_SPLINE_CURVE_WITH_KNOTS('',3,(#57497,#57498,#57499,#57500),
 .UNSPECIFIED.,.F.,.F.,(4,4),(-0.0621213249674689,-0.0358629968300687),
 .UNSPECIFIED.);
#4350=B_SPLINE_CURVE_WITH_KNOTS('',3,(#57502,#57503,#57504,#57505),
 .UNSPECIFIED.,.F.,.F.,(4,4),(0.0934461854545238,0.23169515901548),
 .UNSPECIFIED.);
#4351=B_SPLINE_CURVE_WITH_KNOTS('',3,(#57507,#57508,#57509,#57510),
 .UNSPECIFIED.,.F.,.F.,(4,4),(-1.,-0.380102179092223),.UNSPECIFIED.);
#4352=B_SPLINE_CURVE_WITH_KNOTS('',3,(#57511,#57512,#57513,#57514),
 .UNSPECIFIED.,.F.,.F.,(4,4),(-0.0223584778582685,0.),.UNSPECIFIED.);
#4353=B_SPLINE_CURVE_WITH_KNOTS('',3,(#57518,#57519,#57520,#57521,#57522,
#57523,#57524),.UNSPECIFIED.,.F.,.F.,(4,3,4),(-0.0308504286108605,-0.0276083347051509,
0.),.UNSPECIFIED.);
#4354=B_SPLINE_CURVE_WITH_KNOTS('',3,(#57531,#57532,#57533,#57534,#57535,
#57536),.UNSPECIFIED.,.F.,.F.,(4,2,4),(-0.055805384881149,-0.0275402333550594,
-0.0249547910584523),.UNSPECIFIED.);
#4355=B_SPLINE_CURVE_WITH_KNOTS('',3,(#57539,#57540,#57541,#57542),
 .UNSPECIFIED.,.F.,.F.,(4,4),(-0.221927025840791,-0.0865063411776189),
 .UNSPECIFIED.);
#4356=B_SPLINE_CURVE_WITH_KNOTS('',3,(#57563,#57564,#57565,#57566),
 .UNSPECIFIED.,.F.,.F.,(4,4),(-0.0621213333145467,-0.0358630796440704),
 .UNSPECIFIED.);
#4357=B_SPLINE_CURVE_WITH_KNOTS('',3,(#57568,#57569,#57570,#57571),
 .UNSPECIFIED.,.F.,.F.,(4,4),(0.0934461854545234,0.231695159015479),
 .UNSPECIFIED.);
#4358=B_SPLINE_CURVE_WITH_KNOTS('',3,(#57573,#57574,#57575,#57576),
 .UNSPECIFIED.,.F.,.F.,(4,4),(-1.,-0.380102179092208),.UNSPECIFIED.);
#4359=B_SPLINE_CURVE_WITH_KNOTS('',3,(#57577,#57578,#57579,#57580),
 .UNSPECIFIED.,.F.,.F.,(4,4),(-0.0223585244164941,0.),.UNSPECIFIED.);
#4360=B_SPLINE_CURVE_WITH_KNOTS('',3,(#57602,#57603,#57604,#57605,#57606,
#57607),.UNSPECIFIED.,.F.,.F.,(4,2,4),(0.,0.0279210080669517,0.0559552409499635),
 .UNSPECIFIED.);
#4361=B_SPLINE_CURVE_WITH_KNOTS('',3,(#57633,#57634,#57635,#57636),
 .UNSPECIFIED.,.F.,.F.,(4,4),(0.0934461854545252,0.204724982524033),
 .UNSPECIFIED.);
#4362=B_SPLINE_CURVE_WITH_KNOTS('',3,(#57638,#57639,#57640,#57641),
 .UNSPECIFIED.,.F.,.F.,(4,4),(0.12699083482214,0.265239808385091),
 .UNSPECIFIED.);
#4363=B_SPLINE_CURVE_WITH_KNOTS('',3,(#57643,#57644,#57645,#57646),
 .UNSPECIFIED.,.F.,.F.,(4,4),(0.112193136713498,0.12699083482214),
 .UNSPECIFIED.);
#4364=B_SPLINE_CURVE_WITH_KNOTS('',3,(#57649,#57650,#57651,#57652),
 .UNSPECIFIED.,.F.,.F.,(4,4),(0.231695159015479,0.246492857124062),
 .UNSPECIFIED.);
#4365=B_SPLINE_CURVE_WITH_KNOTS('',3,(#57653,#57654,#57655,#57656),
 .UNSPECIFIED.,.F.,.F.,(4,4),(0.153961011313853,0.265239808385092),
 .UNSPECIFIED.);
#4366=B_SPLINE_CURVE_WITH_KNOTS('',3,(#57670,#57671,#57672,#57673,#57674,
#57675,#57676),.UNSPECIFIED.,.F.,.F.,(4,3,4),(-0.0308504286107679,-0.0276083347050827,
0.),.UNSPECIFIED.);
#4367=B_SPLINE_CURVE_WITH_KNOTS('',3,(#57683,#57684,#57685,#57686,#57687,
#57688),.UNSPECIFIED.,.F.,.F.,(4,2,4),(-0.0558053859642229,-0.0275791003961709,
-0.0249547869966901),.UNSPECIFIED.);
#4368=B_SPLINE_CURVE_WITH_KNOTS('',3,(#57691,#57692,#57693,#57694),
 .UNSPECIFIED.,.F.,.F.,(4,4),(-0.221927025840791,-0.0865063411776191),
 .UNSPECIFIED.);
#4369=B_SPLINE_CURVE_WITH_KNOTS('',3,(#57715,#57716,#57717,#57718),
 .UNSPECIFIED.,.F.,.F.,(4,4),(0.0358629876217305,0.0621213240386919),
 .UNSPECIFIED.);
#4370=B_SPLINE_CURVE_WITH_KNOTS('',3,(#57720,#57721,#57722,#57723),
 .UNSPECIFIED.,.F.,.F.,(4,4),(0.0934461854545239,0.23169515901548),
 .UNSPECIFIED.);
#4371=B_SPLINE_CURVE_WITH_KNOTS('',3,(#57725,#57726,#57727,#57728),
 .UNSPECIFIED.,.F.,.F.,(4,4),(-1.,-0.380102179090426),.UNSPECIFIED.);
#4372=B_SPLINE_CURVE_WITH_KNOTS('',3,(#57729,#57730,#57731,#57732),
 .UNSPECIFIED.,.F.,.F.,(4,4),(-0.0611452087602006,-0.036398080945426),
 .UNSPECIFIED.);
#4373=B_SPLINE_CURVE_WITH_KNOTS('',3,(#57750,#57751,#57752,#57753),
 .UNSPECIFIED.,.F.,.F.,(4,4),(-0.272179652662196,-0.136758967898484),
 .UNSPECIFIED.);
#4374=B_SPLINE_CURVE_WITH_KNOTS('',3,(#57755,#57756,#57757,#57758),
 .UNSPECIFIED.,.F.,.F.,(4,4),(0.,0.0223584778581466),.UNSPECIFIED.);
#4375=B_SPLINE_CURVE_WITH_KNOTS('',3,(#57760,#57761,#57762,#57763),
 .UNSPECIFIED.,.F.,.F.,(4,4),(-1.,-0.380102179090391),.UNSPECIFIED.);
#4376=B_SPLINE_CURVE_WITH_KNOTS('',3,(#57764,#57765,#57766,#57767),
 .UNSPECIFIED.,.F.,.F.,(4,4),(0.126990834822138,0.265239808385089),
 .UNSPECIFIED.);
#4377=B_SPLINE_CURVE_WITH_KNOTS('',3,(#57771,#57772,#57773,#57774,#57775,
#57776,#57777),.UNSPECIFIED.,.F.,.F.,(4,3,4),(-0.030850428610866,-0.0276083347051545,
0.),.UNSPECIFIED.);
#4378=B_SPLINE_CURVE_WITH_KNOTS('',3,(#57784,#57785,#57786,#57787,#57788,
#57789),.UNSPECIFIED.,.F.,.F.,(4,2,4),(-0.0558053859639273,-0.0275791003960369,
-0.024954786996575),.UNSPECIFIED.);
#4379=B_SPLINE_CURVE_WITH_KNOTS('',3,(#57791,#57792,#57793,#57794),
 .UNSPECIFIED.,.F.,.F.,(4,4),(-0.221927025840791,-0.0865063411776187),
 .UNSPECIFIED.);
#4380=B_SPLINE_CURVE_WITH_KNOTS('',3,(#57815,#57816,#57817,#57818),
 .UNSPECIFIED.,.F.,.F.,(4,4),(0.0358629968298236,0.0621213249669539),
 .UNSPECIFIED.);
#4381=B_SPLINE_CURVE_WITH_KNOTS('',3,(#57820,#57821,#57822,#57823),
 .UNSPECIFIED.,.F.,.F.,(4,4),(0.0934461854545234,0.231695159015479),
 .UNSPECIFIED.);
#4382=B_SPLINE_CURVE_WITH_KNOTS('',3,(#57824,#57825,#57826,#57827),
 .UNSPECIFIED.,.F.,.F.,(4,4),(-1.,-0.380102179090419),.UNSPECIFIED.);
#4383=B_SPLINE_CURVE_WITH_KNOTS('',3,(#57845,#57846,#57847,#57848),
 .UNSPECIFIED.,.F.,.F.,(4,4),(-0.272179652662199,-0.136758967898488),
 .UNSPECIFIED.);
#4384=B_SPLINE_CURVE_WITH_KNOTS('',3,(#57850,#57851,#57852,#57853),
 .UNSPECIFIED.,.F.,.F.,(4,4),(0.,0.0223585244163726),.UNSPECIFIED.);
#4385=B_SPLINE_CURVE_WITH_KNOTS('',3,(#57855,#57856,#57857,#57858),
 .UNSPECIFIED.,.F.,.F.,(4,4),(-1.,-0.380102179090403),.UNSPECIFIED.);
#4386=B_SPLINE_CURVE_WITH_KNOTS('',3,(#57859,#57860,#57861,#57862),
 .UNSPECIFIED.,.F.,.F.,(4,4),(0.126990834822142,0.265239808385093),
 .UNSPECIFIED.);
#4387=B_SPLINE_CURVE_WITH_KNOTS('',3,(#57866,#57867,#57868,#57869,#57870,
#57871,#57872),.UNSPECIFIED.,.F.,.F.,(4,3,4),(-0.0308504286107312,-0.0276083347050556,
0.),.UNSPECIFIED.);
#4388=B_SPLINE_CURVE_WITH_KNOTS('',3,(#57879,#57880,#57881,#57882,#57883,
#57884),.UNSPECIFIED.,.F.,.F.,(4,2,4),(-0.0558053859644204,-0.0275791003962489,
-0.0249547869967569),.UNSPECIFIED.);
#4389=B_SPLINE_CURVE_WITH_KNOTS('',3,(#57886,#57887,#57888,#57889),
 .UNSPECIFIED.,.F.,.F.,(4,4),(-0.221927025840791,-0.0865063411776193),
 .UNSPECIFIED.);
#4390=B_SPLINE_CURVE_WITH_KNOTS('',3,(#57910,#57911,#57912,#57913),
 .UNSPECIFIED.,.F.,.F.,(4,4),(-0.0621213333145166,-0.0358630796440529),
 .UNSPECIFIED.);
#4391=B_SPLINE_CURVE_WITH_KNOTS('',3,(#57915,#57916,#57917,#57918),
 .UNSPECIFIED.,.F.,.F.,(4,4),(0.093446185454524,0.231695159015479),
 .UNSPECIFIED.);
#4392=B_SPLINE_CURVE_WITH_KNOTS('',3,(#57919,#57920,#57921,#57922),
 .UNSPECIFIED.,.F.,.F.,(4,4),(-1.,-0.38010217909043),.UNSPECIFIED.);
#4393=B_SPLINE_CURVE_WITH_KNOTS('',3,(#57926,#57927,#57928,#57929,#57930,
#57931,#57932),.UNSPECIFIED.,.F.,.F.,(4,3,4),(-0.0308504336262779,-0.0275666040082405,
0.),.UNSPECIFIED.);
#4394=B_SPLINE_CURVE_WITH_KNOTS('',3,(#57939,#57940,#57941,#57942,#57943,
#57944),.UNSPECIFIED.,.F.,.F.,(4,2,4),(-0.0558053859643313,-0.027579100396226,
-0.0249547870387722),.UNSPECIFIED.);
#4395=B_SPLINE_CURVE_WITH_KNOTS('',3,(#57947,#57948,#57949,#57950),
 .UNSPECIFIED.,.F.,.F.,(4,4),(-0.221927025906161,-0.0865063411775655),
 .UNSPECIFIED.);
#4396=B_SPLINE_CURVE_WITH_KNOTS('',3,(#57970,#57971,#57972,#57973),
 .UNSPECIFIED.,.F.,.F.,(4,4),(-0.0299494398134785,0.),.UNSPECIFIED.);
#4397=B_SPLINE_CURVE_WITH_KNOTS('',3,(#57974,#57975,#57976,#57977,#57978,
#57979),.UNSPECIFIED.,.F.,.F.,(4,2,4),(0.,0.0280015594495552,0.0559551731920623),
 .UNSPECIFIED.);
#4398=B_SPLINE_CURVE_WITH_KNOTS('',3,(#57997,#57998,#57999,#58000),
 .UNSPECIFIED.,.F.,.F.,(4,4),(-0.272179652662197,-0.136758967898486),
 .UNSPECIFIED.);
#4399=B_SPLINE_CURVE_WITH_KNOTS('',3,(#58002,#58003,#58004,#58005),
 .UNSPECIFIED.,.F.,.F.,(4,4),(-0.0611452087600435,-0.036398080945399),
 .UNSPECIFIED.);
#4400=B_SPLINE_CURVE_WITH_KNOTS('',3,(#58006,#58007,#58008,#58009),
 .UNSPECIFIED.,.F.,.F.,(4,4),(-1.,-0.380102179090411),.UNSPECIFIED.);
#4401=B_SPLINE_CURVE_WITH_KNOTS('',3,(#58013,#58014,#58015,#58016,#58017,
#58018,#58019),.UNSPECIFIED.,.F.,.F.,(4,3,4),(-0.0308504286108225,-0.0276083347051228,
0.),.UNSPECIFIED.);
#4402=B_SPLINE_CURVE_WITH_KNOTS('',3,(#58026,#58027,#58028,#58029,#58030,
#58031),.UNSPECIFIED.,.F.,.F.,(4,2,4),(-0.0558053859642228,-0.0275791003961684,
-0.0249547869966877),.UNSPECIFIED.);
#4403=B_SPLINE_CURVE_WITH_KNOTS('',3,(#58033,#58034,#58035,#58036),
 .UNSPECIFIED.,.F.,.F.,(4,4),(-0.221927025840792,-0.0865063411776193),
 .UNSPECIFIED.);
#4404=B_SPLINE_CURVE_WITH_KNOTS('',3,(#58057,#58058,#58059,#58060),
 .UNSPECIFIED.,.F.,.F.,(4,4),(0.0358629876219686,0.0621213240391899),
 .UNSPECIFIED.);
#4405=B_SPLINE_CURVE_WITH_KNOTS('',3,(#58062,#58063,#58064,#58065),
 .UNSPECIFIED.,.F.,.F.,(4,4),(0.0934461854545239,0.23169515901548),
 .UNSPECIFIED.);
#4406=B_SPLINE_CURVE_WITH_KNOTS('',3,(#58066,#58067,#58068,#58069),
 .UNSPECIFIED.,.F.,.F.,(4,4),(-1.,-0.380102179090436),.UNSPECIFIED.);
#4407=B_SPLINE_CURVE_WITH_KNOTS('',3,(#58087,#58088,#58089,#58090),
 .UNSPECIFIED.,.F.,.F.,(4,4),(-0.272179652662196,-0.136758967898484),
 .UNSPECIFIED.);
#4408=B_SPLINE_CURVE_WITH_KNOTS('',3,(#58092,#58093,#58094,#58095),
 .UNSPECIFIED.,.F.,.F.,(4,4),(0.,0.0223584778581942),.UNSPECIFIED.);
#4409=B_SPLINE_CURVE_WITH_KNOTS('',3,(#58097,#58098,#58099,#58100),
 .UNSPECIFIED.,.F.,.F.,(4,4),(-1.,-0.380102179090398),.UNSPECIFIED.);
#4410=B_SPLINE_CURVE_WITH_KNOTS('',3,(#58101,#58102,#58103,#58104),
 .UNSPECIFIED.,.F.,.F.,(4,4),(0.126990834822138,0.265239808385089),
 .UNSPECIFIED.);
#4411=B_SPLINE_CURVE_WITH_KNOTS('',3,(#58108,#58109,#58110,#58111,#58112,
#58113,#58114),.UNSPECIFIED.,.F.,.F.,(4,3,4),(-0.0308504286108342,-0.0276083347051315,
0.),.UNSPECIFIED.);
#4412=B_SPLINE_CURVE_WITH_KNOTS('',3,(#58121,#58122,#58123,#58124,#58125,
#58126),.UNSPECIFIED.,.F.,.F.,(4,2,4),(-0.0558053859641433,-0.0275791003961202,
-0.0249547869966467),.UNSPECIFIED.);
#4413=B_SPLINE_CURVE_WITH_KNOTS('',3,(#58128,#58129,#58130,#58131),
 .UNSPECIFIED.,.F.,.F.,(4,4),(-0.221927025840791,-0.0865063411776189),
 .UNSPECIFIED.);
#4414=B_SPLINE_CURVE_WITH_KNOTS('',3,(#58152,#58153,#58154,#58155),
 .UNSPECIFIED.,.F.,.F.,(4,4),(0.0358629968298035,0.0621213249668936),
 .UNSPECIFIED.);
#4415=B_SPLINE_CURVE_WITH_KNOTS('',3,(#58157,#58158,#58159,#58160),
 .UNSPECIFIED.,.F.,.F.,(4,4),(0.0934461854545236,0.231695159015479),
 .UNSPECIFIED.);
#4416=B_SPLINE_CURVE_WITH_KNOTS('',3,(#58161,#58162,#58163,#58164),
 .UNSPECIFIED.,.F.,.F.,(4,4),(-1.,-0.380102179090424),.UNSPECIFIED.);
#4417=B_SPLINE_CURVE_WITH_KNOTS('',3,(#58182,#58183,#58184,#58185),
 .UNSPECIFIED.,.F.,.F.,(4,4),(-0.2721796526622,-0.136758967898487),
 .UNSPECIFIED.);
#4418=B_SPLINE_CURVE_WITH_KNOTS('',3,(#58187,#58188,#58189,#58190),
 .UNSPECIFIED.,.F.,.F.,(4,4),(0.,0.0223585244163923),.UNSPECIFIED.);
#4419=B_SPLINE_CURVE_WITH_KNOTS('',3,(#58192,#58193,#58194,#58195),
 .UNSPECIFIED.,.F.,.F.,(4,4),(-1.,-0.380102179090384),.UNSPECIFIED.);
#4420=B_SPLINE_CURVE_WITH_KNOTS('',3,(#58196,#58197,#58198,#58199),
 .UNSPECIFIED.,.F.,.F.,(4,4),(0.126990834822142,0.265239808385093),
 .UNSPECIFIED.);
#4421=B_SPLINE_CURVE_WITH_KNOTS('',3,(#58203,#58204,#58205,#58206,#58207,
#58208,#58209),.UNSPECIFIED.,.F.,.F.,(4,3,4),(-0.0308504286108346,-0.0276083347051322,
0.),.UNSPECIFIED.);
#4422=B_SPLINE_CURVE_WITH_KNOTS('',3,(#58216,#58217,#58218,#58219,#58220,
#58221),.UNSPECIFIED.,.F.,.F.,(4,2,4),(-0.055805385964261,-0.0275791003961853,
-0.0249547869967028),.UNSPECIFIED.);
#4423=B_SPLINE_CURVE_WITH_KNOTS('',3,(#58223,#58224,#58225,#58226),
 .UNSPECIFIED.,.F.,.F.,(4,4),(-0.221927025840791,-0.0865063411776194),
 .UNSPECIFIED.);
#4424=B_SPLINE_CURVE_WITH_KNOTS('',3,(#58247,#58248,#58249,#58250),
 .UNSPECIFIED.,.F.,.F.,(4,4),(0.0358630796439579,0.0621213333143259),
 .UNSPECIFIED.);
#4425=B_SPLINE_CURVE_WITH_KNOTS('',3,(#58252,#58253,#58254,#58255),
 .UNSPECIFIED.,.F.,.F.,(4,4),(0.0934461854545242,0.23169515901548),
 .UNSPECIFIED.);
#4426=B_SPLINE_CURVE_WITH_KNOTS('',3,(#58256,#58257,#58258,#58259),
 .UNSPECIFIED.,.F.,.F.,(4,4),(-1.,-0.380102179090412),.UNSPECIFIED.);
#4427=B_SPLINE_CURVE_WITH_KNOTS('',3,(#58276,#58277,#58278,#58279),
 .UNSPECIFIED.,.F.,.F.,(4,4),(-0.272179652662197,-0.136758967898484),
 .UNSPECIFIED.);
#4428=B_SPLINE_CURVE_WITH_KNOTS('',3,(#58281,#58282,#58283,#58284),
 .UNSPECIFIED.,.F.,.F.,(4,4),(-1.,-0.380102179090404),.UNSPECIFIED.);
#4429=B_SPLINE_CURVE_WITH_KNOTS('',3,(#58285,#58286,#58287,#58288),
 .UNSPECIFIED.,.F.,.F.,(4,4),(0.126990834822139,0.26523980838509),
 .UNSPECIFIED.);
#4430=B_SPLINE_CURVE_WITH_KNOTS('',3,(#58306,#58307,#58308,#58309),
 .UNSPECIFIED.,.F.,.F.,(4,4),(0.231695159015479,0.246492857124062),
 .UNSPECIFIED.);
#4431=B_SPLINE_CURVE_WITH_KNOTS('',3,(#58311,#58312,#58313,#58314),
 .UNSPECIFIED.,.F.,.F.,(4,4),(0.,0.000438960297707012),.UNSPECIFIED.);
#4432=B_SPLINE_CURVE_WITH_KNOTS('',3,(#58315,#58316,#58317,#58318,#58319,
#58320,#58321),.UNSPECIFIED.,.F.,.F.,(4,3,4),(0.0223585244163726,0.0288578077806512,
0.0552143212839845),.UNSPECIFIED.);
#4433=B_SPLINE_CURVE_WITH_KNOTS('',3,(#58339,#58340,#58341,#58342),
 .UNSPECIFIED.,.F.,.F.,(4,4),(0.231695159015479,0.246492857124062),
 .UNSPECIFIED.);
#4434=B_SPLINE_CURVE_WITH_KNOTS('',3,(#58344,#58345,#58346,#58347),
 .UNSPECIFIED.,.F.,.F.,(4,4),(0.,0.000438960191917479),.UNSPECIFIED.);
#4435=B_SPLINE_CURVE_WITH_KNOTS('',3,(#58348,#58349,#58350,#58351,#58352,
#58353,#58354),.UNSPECIFIED.,.F.,.F.,(4,3,4),(0.0223584778581466,0.028857534403892,
0.0552146089787789),.UNSPECIFIED.);
#4436=B_SPLINE_CURVE_WITH_KNOTS('',3,(#58372,#58373,#58374,#58375),
 .UNSPECIFIED.,.F.,.F.,(4,4),(0.23169515901548,0.246492857124062),
 .UNSPECIFIED.);
#4437=B_SPLINE_CURVE_WITH_KNOTS('',3,(#58377,#58378,#58379,#58380),
 .UNSPECIFIED.,.F.,.F.,(4,4),(0.,0.000438960107757425),.UNSPECIFIED.);
#4438=B_SPLINE_CURVE_WITH_KNOTS('',3,(#58381,#58382,#58383,#58384,#58385,
#58386,#58387),.UNSPECIFIED.,.F.,.F.,(4,3,4),(-0.036398080945426,-0.0291445555386541,
-0.000145193969552124),.UNSPECIFIED.);
#4439=B_SPLINE_CURVE_WITH_KNOTS('',3,(#58405,#58406,#58407,#58408),
 .UNSPECIFIED.,.F.,.F.,(4,4),(0.23169515901548,0.246492857124062),
 .UNSPECIFIED.);
#4440=B_SPLINE_CURVE_WITH_KNOTS('',3,(#58410,#58411,#58412,#58413),
 .UNSPECIFIED.,.F.,.F.,(4,4),(0.,0.00043896029770756),.UNSPECIFIED.);
#4441=B_SPLINE_CURVE_WITH_KNOTS('',3,(#58414,#58415,#58416,#58417,#58418,
#58419,#58420),.UNSPECIFIED.,.F.,.F.,(4,3,4),(0.0223585244163923,0.0288578077807066,
0.0552143212841931),.UNSPECIFIED.);
#4442=B_SPLINE_CURVE_WITH_KNOTS('',3,(#58438,#58439,#58440,#58441),
 .UNSPECIFIED.,.F.,.F.,(4,4),(0.231695159015479,0.246492857124062),
 .UNSPECIFIED.);
#4443=B_SPLINE_CURVE_WITH_KNOTS('',3,(#58443,#58444,#58445,#58446),
 .UNSPECIFIED.,.F.,.F.,(4,4),(0.,0.00043896019191799),.UNSPECIFIED.);
#4444=B_SPLINE_CURVE_WITH_KNOTS('',3,(#58447,#58448,#58449,#58450,#58451,
#58452,#58453),.UNSPECIFIED.,.F.,.F.,(4,3,4),(0.0223584778581942,0.0288575344040074,
0.0552146089787722),.UNSPECIFIED.);
#4445=B_SPLINE_CURVE_WITH_KNOTS('',3,(#58471,#58472,#58473,#58474),
 .UNSPECIFIED.,.F.,.F.,(4,4),(0.23169515901548,0.246492857124063),
 .UNSPECIFIED.);
#4446=B_SPLINE_CURVE_WITH_KNOTS('',3,(#58476,#58477,#58478,#58479),
 .UNSPECIFIED.,.F.,.F.,(4,4),(0.,0.000438960107757499),.UNSPECIFIED.);
#4447=B_SPLINE_CURVE_WITH_KNOTS('',3,(#58480,#58481,#58482,#58483,#58484,
#58485,#58486),.UNSPECIFIED.,.F.,.F.,(4,3,4),(-0.036398080945399,-0.0291445555386185,
-0.000145193969552187),.UNSPECIFIED.);
#4448=B_SPLINE_CURVE_WITH_KNOTS('',3,(#58503,#58504,#58505,#58506),
 .UNSPECIFIED.,.F.,.F.,(4,4),(-0.272179652662197,-0.136758967898485),
 .UNSPECIFIED.);
#4449=B_SPLINE_CURVE_WITH_KNOTS('',3,(#58508,#58509,#58510,#58511),
 .UNSPECIFIED.,.F.,.F.,(4,4),(-1.,-0.380102179092181),.UNSPECIFIED.);
#4450=B_SPLINE_CURVE_WITH_KNOTS('',3,(#58512,#58513,#58514,#58515),
 .UNSPECIFIED.,.F.,.F.,(4,4),(0.12699083482214,0.26523980838509),
 .UNSPECIFIED.);
#4451=B_SPLINE_CURVE_WITH_KNOTS('',3,(#58533,#58534,#58535,#58536),
 .UNSPECIFIED.,.F.,.F.,(4,4),(0.23169515901548,0.246492857124062),
 .UNSPECIFIED.);
#4452=B_SPLINE_CURVE_WITH_KNOTS('',3,(#58538,#58539,#58540,#58541),
 .UNSPECIFIED.,.F.,.F.,(4,4),(2.71050543121376E-20,0.00043896010775766),
 .UNSPECIFIED.);
#4453=B_SPLINE_CURVE_WITH_KNOTS('',3,(#58542,#58543,#58544,#58545,#58546,
#58547,#58548),.UNSPECIFIED.,.F.,.F.,(4,3,4),(0.000145193969552055,0.0291445555386256,
0.03639808094533),.UNSPECIFIED.);
#4454=B_SPLINE_CURVE_WITH_KNOTS('',3,(#58565,#58566,#58567,#58568),
 .UNSPECIFIED.,.F.,.F.,(4,4),(-0.272179652662198,-0.136758967898486),
 .UNSPECIFIED.);
#4455=B_SPLINE_CURVE_WITH_KNOTS('',3,(#58570,#58571,#58572,#58573),
 .UNSPECIFIED.,.F.,.F.,(4,4),(-1.,-0.380102179092193),.UNSPECIFIED.);
#4456=B_SPLINE_CURVE_WITH_KNOTS('',3,(#58574,#58575,#58576,#58577),
 .UNSPECIFIED.,.F.,.F.,(4,4),(0.12699083482214,0.265239808385091),
 .UNSPECIFIED.);
#4457=B_SPLINE_CURVE_WITH_KNOTS('',3,(#58595,#58596,#58597,#58598),
 .UNSPECIFIED.,.F.,.F.,(4,4),(0.23169515901548,0.246492857124063),
 .UNSPECIFIED.);
#4458=B_SPLINE_CURVE_WITH_KNOTS('',3,(#58600,#58601,#58602,#58603),
 .UNSPECIFIED.,.F.,.F.,(4,4),(0.,0.000438960191917556),.UNSPECIFIED.);
#4459=B_SPLINE_CURVE_WITH_KNOTS('',3,(#58604,#58605,#58606,#58607,#58608,
#58609,#58610),.UNSPECIFIED.,.F.,.F.,(4,3,4),(-0.055214608979223,-0.0288575344040253,
-0.0223584778582685),.UNSPECIFIED.);
#4460=B_SPLINE_CURVE_WITH_KNOTS('',3,(#58627,#58628,#58629,#58630),
 .UNSPECIFIED.,.F.,.F.,(4,4),(-0.272179652662197,-0.136758967898485),
 .UNSPECIFIED.);
#4461=B_SPLINE_CURVE_WITH_KNOTS('',3,(#58632,#58633,#58634,#58635),
 .UNSPECIFIED.,.F.,.F.,(4,4),(-1.,-0.380102179092185),.UNSPECIFIED.);
#4462=B_SPLINE_CURVE_WITH_KNOTS('',3,(#58636,#58637,#58638,#58639),
 .UNSPECIFIED.,.F.,.F.,(4,4),(0.12699083482214,0.26523980838509),
 .UNSPECIFIED.);
#4463=B_SPLINE_CURVE_WITH_KNOTS('',3,(#58657,#58658,#58659,#58660),
 .UNSPECIFIED.,.F.,.F.,(4,4),(0.,0.000438960297707225),.UNSPECIFIED.);
#4464=B_SPLINE_CURVE_WITH_KNOTS('',3,(#58661,#58662,#58663,#58664,#58665,
#58666,#58667),.UNSPECIFIED.,.F.,.F.,(4,3,4),(-0.0552143212843298,-0.0288578077807816,
-0.0223585244164941),.UNSPECIFIED.);
#4465=B_SPLINE_CURVE_WITH_KNOTS('',3,(#58684,#58685,#58686,#58687),
 .UNSPECIFIED.,.F.,.F.,(4,4),(-0.272179652662254,-0.136758967931396),
 .UNSPECIFIED.);
#4466=B_SPLINE_CURVE_WITH_KNOTS('',3,(#58705,#58706,#58707,#58708),
 .UNSPECIFIED.,.F.,.F.,(4,4),(0.149113104129392,0.14946619853298),
 .UNSPECIFIED.);
#4467=B_SPLINE_CURVE_WITH_KNOTS('',3,(#58709,#58710,#58711,#58712),
 .UNSPECIFIED.,.F.,.F.,(4,4),(0.112193136713498,0.12699083482214),
 .UNSPECIFIED.);
#4468=B_SPLINE_CURVE_WITH_KNOTS('',3,(#58730,#58731,#58732,#58733),
 .UNSPECIFIED.,.F.,.F.,(4,4),(0.149111564070519,0.149464659958529),
 .UNSPECIFIED.);
#4469=B_SPLINE_CURVE_WITH_KNOTS('',3,(#58734,#58735,#58736,#58737),
 .UNSPECIFIED.,.F.,.F.,(4,4),(0.112193136713498,0.12699083482214),
 .UNSPECIFIED.);
#4470=B_SPLINE_CURVE_WITH_KNOTS('',3,(#58755,#58756,#58757,#58758),
 .UNSPECIFIED.,.F.,.F.,(4,4),(0.149109634661021,0.149462732410104),
 .UNSPECIFIED.);
#4471=B_SPLINE_CURVE_WITH_KNOTS('',3,(#58759,#58760,#58761,#58762),
 .UNSPECIFIED.,.F.,.F.,(4,4),(0.112193136713498,0.12699083482214),
 .UNSPECIFIED.);
#4472=B_SPLINE_CURVE_WITH_KNOTS('',3,(#58779,#58780,#58781,#58782),
 .UNSPECIFIED.,.F.,.F.,(4,4),(0.149109634661038,0.149462732410121),
 .UNSPECIFIED.);
#4473=B_SPLINE_CURVE_WITH_KNOTS('',3,(#58800,#58801,#58802,#58803),
 .UNSPECIFIED.,.F.,.F.,(4,4),(0.149111564070538,0.149464659958548),
 .UNSPECIFIED.);
#4474=B_SPLINE_CURVE_WITH_KNOTS('',3,(#58804,#58805,#58806,#58807),
 .UNSPECIFIED.,.F.,.F.,(4,4),(0.112193136713496,0.126990834822138),
 .UNSPECIFIED.);
#4475=B_SPLINE_CURVE_WITH_KNOTS('',3,(#58825,#58826,#58827,#58828),
 .UNSPECIFIED.,.F.,.F.,(4,4),(0.149113104129386,0.149466198532974),
 .UNSPECIFIED.);
#4476=B_SPLINE_CURVE_WITH_KNOTS('',3,(#58829,#58830,#58831,#58832),
 .UNSPECIFIED.,.F.,.F.,(4,4),(0.1121931367135,0.126990834822142),
 .UNSPECIFIED.);
#4477=B_SPLINE_CURVE_WITH_KNOTS('',3,(#58850,#58851,#58852,#58853),
 .UNSPECIFIED.,.F.,.F.,(4,4),(0.14910963466104,0.149462732410123),
 .UNSPECIFIED.);
#4478=B_SPLINE_CURVE_WITH_KNOTS('',3,(#58854,#58855,#58856,#58857),
 .UNSPECIFIED.,.F.,.F.,(4,4),(0.112193136713497,0.126990834822139),
 .UNSPECIFIED.);
#4479=B_SPLINE_CURVE_WITH_KNOTS('',3,(#58875,#58876,#58877,#58878),
 .UNSPECIFIED.,.F.,.F.,(4,4),(0.149111564070554,0.149464659958564),
 .UNSPECIFIED.);
#4480=B_SPLINE_CURVE_WITH_KNOTS('',3,(#58879,#58880,#58881,#58882),
 .UNSPECIFIED.,.F.,.F.,(4,4),(0.112193136713496,0.126990834822138),
 .UNSPECIFIED.);
#4481=B_SPLINE_CURVE_WITH_KNOTS('',3,(#58900,#58901,#58902,#58903),
 .UNSPECIFIED.,.F.,.F.,(4,4),(0.149113104129403,0.149466198532991),
 .UNSPECIFIED.);
#4482=B_SPLINE_CURVE_WITH_KNOTS('',3,(#58904,#58905,#58906,#58907),
 .UNSPECIFIED.,.F.,.F.,(4,4),(0.112193136713501,0.126990834822142),
 .UNSPECIFIED.);
#5356=LINE('',#57394,#6768);
#5357=LINE('',#57396,#6769);
#5358=LINE('',#57398,#6770);
#5359=LINE('',#57412,#6771);
#5360=LINE('',#57413,#6772);
#5361=LINE('',#57460,#6773);
#5362=LINE('',#57462,#6774);
#5363=LINE('',#57464,#6775);
#5364=LINE('',#57478,#6776);
#5365=LINE('',#57479,#6777);
#5366=LINE('',#57526,#6778);
#5367=LINE('',#57528,#6779);
#5368=LINE('',#57530,#6780);
#5369=LINE('',#57544,#6781);
#5370=LINE('',#57545,#6782);
#5371=LINE('',#57588,#6783);
#5372=LINE('',#57590,#6784);
#5373=LINE('',#57591,#6785);
#5374=LINE('',#57609,#6786);
#5375=LINE('',#57610,#6787);
#5376=LINE('',#57659,#6788);
#5377=LINE('',#57661,#6789);
#5378=LINE('',#57662,#6790);
#5379=LINE('',#57665,#6791);
#5380=LINE('',#57666,#6792);
#5381=LINE('',#57678,#6793);
#5382=LINE('',#57680,#6794);
#5383=LINE('',#57682,#6795);
#5384=LINE('',#57696,#6796);
#5385=LINE('',#57697,#6797);
#5386=LINE('',#57779,#6798);
#5387=LINE('',#57781,#6799);
#5388=LINE('',#57783,#6800);
#5389=LINE('',#57796,#6801);
#5390=LINE('',#57797,#6802);
#5391=LINE('',#57874,#6803);
#5392=LINE('',#57876,#6804);
#5393=LINE('',#57878,#6805);
#5394=LINE('',#57891,#6806);
#5395=LINE('',#57892,#6807);
#5396=LINE('',#57934,#6808);
#5397=LINE('',#57936,#6809);
#5398=LINE('',#57938,#6810);
#5399=LINE('',#57952,#6811);
#5400=LINE('',#57953,#6812);
#5401=LINE('',#58021,#6813);
#5402=LINE('',#58023,#6814);
#5403=LINE('',#58025,#6815);
#5404=LINE('',#58038,#6816);
#5405=LINE('',#58039,#6817);
#5406=LINE('',#58116,#6818);
#5407=LINE('',#58118,#6819);
#5408=LINE('',#58120,#6820);
#5409=LINE('',#58133,#6821);
#5410=LINE('',#58134,#6822);
#5411=LINE('',#58211,#6823);
#5412=LINE('',#58213,#6824);
#5413=LINE('',#58215,#6825);
#5414=LINE('',#58228,#6826);
#5415=LINE('',#58229,#6827);
#5416=LINE('',#58909,#6828);
#5417=LINE('',#58911,#6829);
#5418=LINE('',#58913,#6830);
#5419=LINE('',#58915,#6831);
#5420=LINE('',#58938,#6832);
#5421=LINE('',#58943,#6833);
#5422=LINE('',#58946,#6834);
#5423=LINE('',#58948,#6835);
#5424=LINE('',#58950,#6836);
#5425=LINE('',#58952,#6837);
#5426=LINE('',#58954,#6838);
#5427=LINE('',#58956,#6839);
#5428=LINE('',#58958,#6840);
#5429=LINE('',#58960,#6841);
#5430=LINE('',#58962,#6842);
#5431=LINE('',#58969,#6843);
#5432=LINE('',#58973,#6844);
#5433=LINE('',#58977,#6845);
#6768=VECTOR('',#22438,10.);
#6769=VECTOR('',#22439,10.);
#6770=VECTOR('',#22440,10.);
#6771=VECTOR('',#22443,10.);
#6772=VECTOR('',#22444,10.);
#6773=VECTOR('',#22447,10.);
#6774=VECTOR('',#22448,10.);
#6775=VECTOR('',#22449,10.);
#6776=VECTOR('',#22452,10.);
#6777=VECTOR('',#22453,10.);
#6778=VECTOR('',#22456,10.);
#6779=VECTOR('',#22457,10.);
#6780=VECTOR('',#22458,10.);
#6781=VECTOR('',#22461,10.);
#6782=VECTOR('',#22462,10.);
#6783=VECTOR('',#22465,10.);
#6784=VECTOR('',#22466,10.);
#6785=VECTOR('',#22467,10.);
#6786=VECTOR('',#22470,10.);
#6787=VECTOR('',#22471,10.);
#6788=VECTOR('',#22478,10.);
#6789=VECTOR('',#22479,10.);
#6790=VECTOR('',#22480,10.);
#6791=VECTOR('',#22483,10.);
#6792=VECTOR('',#22484,10.);
#6793=VECTOR('',#22487,10.);
#6794=VECTOR('',#22488,10.);
#6795=VECTOR('',#22489,10.);
#6796=VECTOR('',#22492,10.);
#6797=VECTOR('',#22493,10.);
#6798=VECTOR('',#22496,10.);
#6799=VECTOR('',#22497,10.);
#6800=VECTOR('',#22498,10.);
#6801=VECTOR('',#22501,10.);
#6802=VECTOR('',#22502,10.);
#6803=VECTOR('',#22505,10.);
#6804=VECTOR('',#22506,10.);
#6805=VECTOR('',#22507,10.);
#6806=VECTOR('',#22510,10.);
#6807=VECTOR('',#22511,10.);
#6808=VECTOR('',#22514,10.);
#6809=VECTOR('',#22515,10.);
#6810=VECTOR('',#22516,10.);
#6811=VECTOR('',#22519,10.);
#6812=VECTOR('',#22520,10.);
#6813=VECTOR('',#22523,10.);
#6814=VECTOR('',#22524,10.);
#6815=VECTOR('',#22525,10.);
#6816=VECTOR('',#22528,10.);
#6817=VECTOR('',#22529,10.);
#6818=VECTOR('',#22532,10.);
#6819=VECTOR('',#22533,10.);
#6820=VECTOR('',#22534,10.);
#6821=VECTOR('',#22537,10.);
#6822=VECTOR('',#22538,10.);
#6823=VECTOR('',#22541,10.);
#6824=VECTOR('',#22542,10.);
#6825=VECTOR('',#22543,10.);
#6826=VECTOR('',#22546,10.);
#6827=VECTOR('',#22547,10.);
#6828=VECTOR('',#22550,10.);
#6829=VECTOR('',#22553,10.);
#6830=VECTOR('',#22556,10.);
#6831=VECTOR('',#22559,10.);
#6832=VECTOR('',#22600,3.8);
#6833=VECTOR('',#22605,3.8);
#6834=VECTOR('',#22610,10.);
#6835=VECTOR('',#22613,10.);
#6836=VECTOR('',#22616,10.);
#6837=VECTOR('',#22619,10.);
#6838=VECTOR('',#22622,10.);
#6839=VECTOR('',#22625,10.);
#6840=VECTOR('',#22628,10.);
#6841=VECTOR('',#22631,10.);
#6842=VECTOR('',#22634,3.55);
#6843=VECTOR('',#22643,6.35);
#6844=VECTOR('',#22648,6.5);
#6845=VECTOR('',#22653,6.25);
#8604=VERTEX_POINT('',#57384);
#8605=VERTEX_POINT('',#57385);
#8606=VERTEX_POINT('',#57393);
#8607=VERTEX_POINT('',#57395);
#8608=VERTEX_POINT('',#57397);
#8609=VERTEX_POINT('',#57406);
#8610=VERTEX_POINT('',#57411);
#8611=VERTEX_POINT('',#57430);
#8612=VERTEX_POINT('',#57435);
#8613=VERTEX_POINT('',#57440);
#8614=VERTEX_POINT('',#57450);
#8615=VERTEX_POINT('',#57451);
#8616=VERTEX_POINT('',#57459);
#8617=VERTEX_POINT('',#57461);
#8618=VERTEX_POINT('',#57463);
#8619=VERTEX_POINT('',#57472);
#8620=VERTEX_POINT('',#57477);
#8621=VERTEX_POINT('',#57496);
#8622=VERTEX_POINT('',#57501);
#8623=VERTEX_POINT('',#57506);
#8624=VERTEX_POINT('',#57516);
#8625=VERTEX_POINT('',#57517);
#8626=VERTEX_POINT('',#57525);
#8627=VERTEX_POINT('',#57527);
#8628=VERTEX_POINT('',#57529);
#8629=VERTEX_POINT('',#57538);
#8630=VERTEX_POINT('',#57543);
#8631=VERTEX_POINT('',#57562);
#8632=VERTEX_POINT('',#57567);
#8633=VERTEX_POINT('',#57572);
#8634=VERTEX_POINT('',#57582);
#8635=VERTEX_POINT('',#57583);
#8636=VERTEX_POINT('',#57587);
#8637=VERTEX_POINT('',#57589);
#8638=VERTEX_POINT('',#57593);
#8639=VERTEX_POINT('',#57597);
#8640=VERTEX_POINT('',#57601);
#8641=VERTEX_POINT('',#57608);
#8642=VERTEX_POINT('',#57612);
#8643=VERTEX_POINT('',#57616);
#8644=VERTEX_POINT('',#57620);
#8645=VERTEX_POINT('',#57624);
#8646=VERTEX_POINT('',#57628);
#8647=VERTEX_POINT('',#57632);
#8648=VERTEX_POINT('',#57637);
#8649=VERTEX_POINT('',#57642);
#8650=VERTEX_POINT('',#57647);
#8651=VERTEX_POINT('',#57658);
#8652=VERTEX_POINT('',#57660);
#8653=VERTEX_POINT('',#57664);
#8654=VERTEX_POINT('',#57668);
#8655=VERTEX_POINT('',#57669);
#8656=VERTEX_POINT('',#57677);
#8657=VERTEX_POINT('',#57679);
#8658=VERTEX_POINT('',#57681);
#8659=VERTEX_POINT('',#57690);
#8660=VERTEX_POINT('',#57695);
#8661=VERTEX_POINT('',#57714);
#8662=VERTEX_POINT('',#57719);
#8663=VERTEX_POINT('',#57724);
#8664=VERTEX_POINT('',#57749);
#8665=VERTEX_POINT('',#57754);
#8666=VERTEX_POINT('',#57759);
#8667=VERTEX_POINT('',#57769);
#8668=VERTEX_POINT('',#57770);
#8669=VERTEX_POINT('',#57778);
#8670=VERTEX_POINT('',#57780);
#8671=VERTEX_POINT('',#57782);
#8672=VERTEX_POINT('',#57795);
#8673=VERTEX_POINT('',#57814);
#8674=VERTEX_POINT('',#57819);
#8675=VERTEX_POINT('',#57844);
#8676=VERTEX_POINT('',#57849);
#8677=VERTEX_POINT('',#57854);
#8678=VERTEX_POINT('',#57864);
#8679=VERTEX_POINT('',#57865);
#8680=VERTEX_POINT('',#57873);
#8681=VERTEX_POINT('',#57875);
#8682=VERTEX_POINT('',#57877);
#8683=VERTEX_POINT('',#57890);
#8684=VERTEX_POINT('',#57909);
#8685=VERTEX_POINT('',#57914);
#8686=VERTEX_POINT('',#57924);
#8687=VERTEX_POINT('',#57925);
#8688=VERTEX_POINT('',#57933);
#8689=VERTEX_POINT('',#57935);
#8690=VERTEX_POINT('',#57937);
#8691=VERTEX_POINT('',#57946);
#8692=VERTEX_POINT('',#57951);
#8693=VERTEX_POINT('',#57996);
#8694=VERTEX_POINT('',#58001);
#8695=VERTEX_POINT('',#58011);
#8696=VERTEX_POINT('',#58012);
#8697=VERTEX_POINT('',#58020);
#8698=VERTEX_POINT('',#58022);
#8699=VERTEX_POINT('',#58024);
#8700=VERTEX_POINT('',#58037);
#8701=VERTEX_POINT('',#58056);
#8702=VERTEX_POINT('',#58061);
#8703=VERTEX_POINT('',#58086);
#8704=VERTEX_POINT('',#58091);
#8705=VERTEX_POINT('',#58096);
#8706=VERTEX_POINT('',#58106);
#8707=VERTEX_POINT('',#58107);
#8708=VERTEX_POINT('',#58115);
#8709=VERTEX_POINT('',#58117);
#8710=VERTEX_POINT('',#58119);
#8711=VERTEX_POINT('',#58132);
#8712=VERTEX_POINT('',#58151);
#8713=VERTEX_POINT('',#58156);
#8714=VERTEX_POINT('',#58181);
#8715=VERTEX_POINT('',#58186);
#8716=VERTEX_POINT('',#58191);
#8717=VERTEX_POINT('',#58201);
#8718=VERTEX_POINT('',#58202);
#8719=VERTEX_POINT('',#58210);
#8720=VERTEX_POINT('',#58212);
#8721=VERTEX_POINT('',#58214);
#8722=VERTEX_POINT('',#58227);
#8723=VERTEX_POINT('',#58246);
#8724=VERTEX_POINT('',#58251);
#8725=VERTEX_POINT('',#58280);
#8726=VERTEX_POINT('',#58305);
#8727=VERTEX_POINT('',#58310);
#8728=VERTEX_POINT('',#58338);
#8729=VERTEX_POINT('',#58343);
#8730=VERTEX_POINT('',#58371);
#8731=VERTEX_POINT('',#58376);
#8732=VERTEX_POINT('',#58404);
#8733=VERTEX_POINT('',#58409);
#8734=VERTEX_POINT('',#58437);
#8735=VERTEX_POINT('',#58442);
#8736=VERTEX_POINT('',#58470);
#8737=VERTEX_POINT('',#58475);
#8738=VERTEX_POINT('',#58507);
#8739=VERTEX_POINT('',#58532);
#8740=VERTEX_POINT('',#58537);
#8741=VERTEX_POINT('',#58569);
#8742=VERTEX_POINT('',#58594);
#8743=VERTEX_POINT('',#58599);
#8744=VERTEX_POINT('',#58631);
#8745=VERTEX_POINT('',#58656);
#8746=VERTEX_POINT('',#58704);
#8747=VERTEX_POINT('',#58729);
#8748=VERTEX_POINT('',#58754);
#8749=VERTEX_POINT('',#58799);
#8750=VERTEX_POINT('',#58824);
#8751=VERTEX_POINT('',#58849);
#8752=VERTEX_POINT('',#58874);
#8753=VERTEX_POINT('',#58899);
#8754=VERTEX_POINT('',#58925);
#8755=VERTEX_POINT('',#58936);
#8756=VERTEX_POINT('',#58940);
#8757=VERTEX_POINT('',#58942);
#8758=VERTEX_POINT('',#58964);
#8759=VERTEX_POINT('',#58967);
#8760=VERTEX_POINT('',#58971);
#8761=VERTEX_POINT('',#58975);
#11037=EDGE_CURVE('',#8604,#8605,#4339,.T.);
#11038=EDGE_CURVE('',#8605,#8606,#5356,.T.);
#11039=EDGE_CURVE('',#8606,#8607,#5357,.F.);
#11040=EDGE_CURVE('',#8607,#8608,#5358,.T.);
#11041=EDGE_CURVE('',#8608,#8604,#4340,.T.);
#11042=EDGE_CURVE('',#8609,#8605,#4341,.T.);
#11043=EDGE_CURVE('',#8610,#8609,#5359,.T.);
#11044=EDGE_CURVE('',#8606,#8610,#5360,.T.);
#11045=EDGE_CURVE('',#8611,#8604,#4342,.T.);
#11046=EDGE_CURVE('',#8611,#8612,#4343,.T.);
#11047=EDGE_CURVE('',#8612,#8613,#4344,.T.);
#11048=EDGE_CURVE('',#8613,#8609,#4345,.T.);
#11049=EDGE_CURVE('',#8614,#8615,#4346,.T.);
#11050=EDGE_CURVE('',#8615,#8616,#5361,.T.);
#11051=EDGE_CURVE('',#8616,#8617,#5362,.F.);
#11052=EDGE_CURVE('',#8617,#8618,#5363,.T.);
#11053=EDGE_CURVE('',#8618,#8614,#4347,.T.);
#11054=EDGE_CURVE('',#8619,#8615,#4348,.T.);
#11055=EDGE_CURVE('',#8620,#8619,#5364,.T.);
#11056=EDGE_CURVE('',#8616,#8620,#5365,.T.);
#11057=EDGE_CURVE('',#8621,#8614,#4349,.T.);
#11058=EDGE_CURVE('',#8621,#8622,#4350,.T.);
#11059=EDGE_CURVE('',#8622,#8623,#4351,.T.);
#11060=EDGE_CURVE('',#8623,#8619,#4352,.T.);
#11061=EDGE_CURVE('',#8624,#8625,#4353,.T.);
#11062=EDGE_CURVE('',#8625,#8626,#5366,.T.);
#11063=EDGE_CURVE('',#8626,#8627,#5367,.F.);
#11064=EDGE_CURVE('',#8627,#8628,#5368,.T.);
#11065=EDGE_CURVE('',#8628,#8624,#4354,.T.);
#11066=EDGE_CURVE('',#8629,#8625,#4355,.T.);
#11067=EDGE_CURVE('',#8630,#8629,#5369,.T.);
#11068=EDGE_CURVE('',#8626,#8630,#5370,.T.);
#11069=EDGE_CURVE('',#8631,#8624,#4356,.T.);
#11070=EDGE_CURVE('',#8631,#8632,#4357,.T.);
#11071=EDGE_CURVE('',#8632,#8633,#4358,.T.);
#11072=EDGE_CURVE('',#8633,#8629,#4359,.T.);
#11073=EDGE_CURVE('',#8634,#8635,#1056,.T.);
#11074=EDGE_CURVE('',#8635,#8636,#5371,.T.);
#11075=EDGE_CURVE('',#8636,#8637,#5372,.F.);
#11076=EDGE_CURVE('',#8637,#8634,#5373,.T.);
#11077=EDGE_CURVE('',#8635,#8638,#1057,.T.);
#11078=EDGE_CURVE('',#8638,#8639,#1058,.T.);
#11079=EDGE_CURVE('',#8640,#8639,#4360,.F.);
#11080=EDGE_CURVE('',#8641,#8640,#5374,.T.);
#11081=EDGE_CURVE('',#8636,#8641,#5375,.T.);
#11082=EDGE_CURVE('',#8642,#8634,#1059,.T.);
#11083=EDGE_CURVE('',#8643,#8642,#1060,.T.);
#11084=EDGE_CURVE('',#8644,#8643,#1061,.T.);
#11085=EDGE_CURVE('',#8645,#8644,#1062,.T.);
#11086=EDGE_CURVE('',#8646,#8645,#1063,.T.);
#11087=EDGE_CURVE('',#8647,#8646,#4361,.T.);
#11088=EDGE_CURVE('',#8648,#8647,#4362,.T.);
#11089=EDGE_CURVE('',#8649,#8648,#4363,.T.);
#11090=EDGE_CURVE('',#8650,#8649,#3652,.T.);
#11091=EDGE_CURVE('',#8632,#8650,#4364,.T.);
#11092=EDGE_CURVE('',#8639,#8631,#4365,.T.);
#11093=EDGE_CURVE('',#8643,#8651,#5376,.T.);
#11094=EDGE_CURVE('',#8651,#8652,#5377,.F.);
#11095=EDGE_CURVE('',#8652,#8644,#5378,.T.);
#11096=EDGE_CURVE('',#8653,#8642,#5379,.T.);
#11097=EDGE_CURVE('',#8651,#8653,#5380,.T.);
#11098=EDGE_CURVE('',#8654,#8655,#4366,.T.);
#11099=EDGE_CURVE('',#8655,#8656,#5381,.T.);
#11100=EDGE_CURVE('',#8656,#8657,#5382,.F.);
#11101=EDGE_CURVE('',#8657,#8658,#5383,.T.);
#11102=EDGE_CURVE('',#8658,#8654,#4367,.T.);
#11103=EDGE_CURVE('',#8659,#8655,#4368,.T.);
#11104=EDGE_CURVE('',#8660,#8659,#5384,.T.);
#11105=EDGE_CURVE('',#8656,#8660,#5385,.T.);
#11106=EDGE_CURVE('',#8654,#8661,#4369,.T.);
#11107=EDGE_CURVE('',#8661,#8662,#4370,.T.);
#11108=EDGE_CURVE('',#8662,#8663,#4371,.T.);
#11109=EDGE_CURVE('',#8659,#8663,#4372,.T.);
#11110=EDGE_CURVE('',#8658,#8664,#4373,.T.);
#11111=EDGE_CURVE('',#8664,#8665,#4374,.T.);
#11112=EDGE_CURVE('',#8666,#8665,#4375,.T.);
#11113=EDGE_CURVE('',#8666,#8661,#4376,.T.);
#11114=EDGE_CURVE('',#8667,#8668,#4377,.T.);
#11115=EDGE_CURVE('',#8668,#8669,#5386,.T.);
#11116=EDGE_CURVE('',#8669,#8670,#5387,.F.);
#11117=EDGE_CURVE('',#8670,#8671,#5388,.T.);
#11118=EDGE_CURVE('',#8671,#8667,#4378,.T.);
#11119=EDGE_CURVE('',#8664,#8668,#4379,.T.);
#11120=EDGE_CURVE('',#8672,#8664,#5389,.T.);
#11121=EDGE_CURVE('',#8669,#8672,#5390,.T.);
#11122=EDGE_CURVE('',#8667,#8673,#4380,.T.);
#11123=EDGE_CURVE('',#8673,#8674,#4381,.T.);
#11124=EDGE_CURVE('',#8674,#8665,#4382,.T.);
#11125=EDGE_CURVE('',#8671,#8675,#4383,.T.);
#11126=EDGE_CURVE('',#8675,#8676,#4384,.T.);
#11127=EDGE_CURVE('',#8677,#8676,#4385,.T.);
#11128=EDGE_CURVE('',#8677,#8673,#4386,.T.);
#11129=EDGE_CURVE('',#8678,#8679,#4387,.T.);
#11130=EDGE_CURVE('',#8679,#8680,#5391,.T.);
#11131=EDGE_CURVE('',#8680,#8681,#5392,.F.);
#11132=EDGE_CURVE('',#8681,#8682,#5393,.T.);
#11133=EDGE_CURVE('',#8682,#8678,#4388,.T.);
#11134=EDGE_CURVE('',#8675,#8679,#4389,.T.);
#11135=EDGE_CURVE('',#8683,#8675,#5394,.T.);
#11136=EDGE_CURVE('',#8680,#8683,#5395,.T.);
#11137=EDGE_CURVE('',#8684,#8678,#4390,.T.);
#11138=EDGE_CURVE('',#8684,#8685,#4391,.T.);
#11139=EDGE_CURVE('',#8685,#8676,#4392,.T.);
#11140=EDGE_CURVE('',#8686,#8687,#4393,.T.);
#11141=EDGE_CURVE('',#8687,#8688,#5396,.T.);
#11142=EDGE_CURVE('',#8688,#8689,#5397,.F.);
#11143=EDGE_CURVE('',#8689,#8690,#5398,.T.);
#11144=EDGE_CURVE('',#8690,#8686,#4394,.T.);
#11145=EDGE_CURVE('',#8691,#8687,#4395,.T.);
#11146=EDGE_CURVE('',#8692,#8691,#5399,.T.);
#11147=EDGE_CURVE('',#8688,#8692,#5400,.T.);
#11148=EDGE_CURVE('',#8686,#8647,#4396,.T.);
#11149=EDGE_CURVE('',#8646,#8691,#4397,.F.);
#11150=EDGE_CURVE('',#8690,#8693,#4398,.T.);
#11151=EDGE_CURVE('',#8693,#8694,#4399,.T.);
#11152=EDGE_CURVE('',#8648,#8694,#4400,.T.);
#11153=EDGE_CURVE('',#8695,#8696,#4401,.T.);
#11154=EDGE_CURVE('',#8696,#8697,#5401,.T.);
#11155=EDGE_CURVE('',#8697,#8698,#5402,.F.);
#11156=EDGE_CURVE('',#8698,#8699,#5403,.T.);
#11157=EDGE_CURVE('',#8699,#8695,#4402,.T.);
#11158=EDGE_CURVE('',#8693,#8696,#4403,.T.);
#11159=EDGE_CURVE('',#8700,#8693,#5404,.T.);
#11160=EDGE_CURVE('',#8697,#8700,#5405,.T.);
#11161=EDGE_CURVE('',#8695,#8701,#4404,.T.);
#11162=EDGE_CURVE('',#8701,#8702,#4405,.T.);
#11163=EDGE_CURVE('',#8702,#8694,#4406,.T.);
#11164=EDGE_CURVE('',#8699,#8703,#4407,.T.);
#11165=EDGE_CURVE('',#8703,#8704,#4408,.T.);
#11166=EDGE_CURVE('',#8705,#8704,#4409,.T.);
#11167=EDGE_CURVE('',#8705,#8701,#4410,.T.);
#11168=EDGE_CURVE('',#8706,#8707,#4411,.T.);
#11169=EDGE_CURVE('',#8707,#8708,#5406,.T.);
#11170=EDGE_CURVE('',#8708,#8709,#5407,.F.);
#11171=EDGE_CURVE('',#8709,#8710,#5408,.T.);
#11172=EDGE_CURVE('',#8710,#8706,#4412,.T.);
#11173=EDGE_CURVE('',#8703,#8707,#4413,.T.);
#11174=EDGE_CURVE('',#8711,#8703,#5409,.T.);
#11175=EDGE_CURVE('',#8708,#8711,#5410,.T.);
#11176=EDGE_CURVE('',#8706,#8712,#4414,.T.);
#11177=EDGE_CURVE('',#8712,#8713,#4415,.T.);
#11178=EDGE_CURVE('',#8713,#8704,#4416,.T.);
#11179=EDGE_CURVE('',#8710,#8714,#4417,.T.);
#11180=EDGE_CURVE('',#8714,#8715,#4418,.T.);
#11181=EDGE_CURVE('',#8716,#8715,#4419,.T.);
#11182=EDGE_CURVE('',#8716,#8712,#4420,.T.);
#11183=EDGE_CURVE('',#8717,#8718,#4421,.T.);
#11184=EDGE_CURVE('',#8718,#8719,#5411,.T.);
#11185=EDGE_CURVE('',#8719,#8720,#5412,.F.);
#11186=EDGE_CURVE('',#8720,#8721,#5413,.T.);
#11187=EDGE_CURVE('',#8721,#8717,#4422,.T.);
#11188=EDGE_CURVE('',#8714,#8718,#4423,.T.);
#11189=EDGE_CURVE('',#8722,#8714,#5414,.T.);
#11190=EDGE_CURVE('',#8719,#8722,#5415,.T.);
#11191=EDGE_CURVE('',#8717,#8723,#4424,.T.);
#11192=EDGE_CURVE('',#8723,#8724,#4425,.T.);
#11193=EDGE_CURVE('',#8724,#8715,#4426,.T.);
#11194=EDGE_CURVE('',#8721,#8659,#4427,.T.);
#11195=EDGE_CURVE('',#8725,#8663,#4428,.T.);
#11196=EDGE_CURVE('',#8725,#8723,#4429,.T.);
#11197=EDGE_CURVE('',#8685,#8726,#4430,.T.);
#11198=EDGE_CURVE('',#8726,#8727,#4431,.T.);
#11199=EDGE_CURVE('',#8676,#8727,#4432,.T.);
#11200=EDGE_CURVE('',#8674,#8728,#4433,.T.);
#11201=EDGE_CURVE('',#8728,#8729,#4434,.T.);
#11202=EDGE_CURVE('',#8665,#8729,#4435,.T.);
#11203=EDGE_CURVE('',#8662,#8730,#4436,.T.);
#11204=EDGE_CURVE('',#8730,#8731,#4437,.T.);
#11205=EDGE_CURVE('',#8663,#8731,#4438,.T.);
#11206=EDGE_CURVE('',#8724,#8732,#4439,.T.);
#11207=EDGE_CURVE('',#8732,#8733,#4440,.T.);
#11208=EDGE_CURVE('',#8715,#8733,#4441,.T.);
#11209=EDGE_CURVE('',#8713,#8734,#4442,.T.);
#11210=EDGE_CURVE('',#8734,#8735,#4443,.T.);
#11211=EDGE_CURVE('',#8704,#8735,#4444,.T.);
#11212=EDGE_CURVE('',#8702,#8736,#4445,.T.);
#11213=EDGE_CURVE('',#8736,#8737,#4446,.T.);
#11214=EDGE_CURVE('',#8694,#8737,#4447,.T.);
#11215=EDGE_CURVE('',#8682,#8609,#4448,.T.);
#11216=EDGE_CURVE('',#8738,#8613,#4449,.T.);
#11217=EDGE_CURVE('',#8738,#8684,#4450,.T.);
#11218=EDGE_CURVE('',#8612,#8739,#4451,.T.);
#11219=EDGE_CURVE('',#8739,#8740,#4452,.T.);
#11220=EDGE_CURVE('',#8740,#8613,#4453,.T.);
#11221=EDGE_CURVE('',#8608,#8619,#4454,.T.);
#11222=EDGE_CURVE('',#8741,#8623,#4455,.T.);
#11223=EDGE_CURVE('',#8741,#8611,#4456,.T.);
#11224=EDGE_CURVE('',#8622,#8742,#4457,.T.);
#11225=EDGE_CURVE('',#8742,#8743,#4458,.T.);
#11226=EDGE_CURVE('',#8743,#8623,#4459,.T.);
#11227=EDGE_CURVE('',#8618,#8629,#4460,.T.);
#11228=EDGE_CURVE('',#8744,#8633,#4461,.T.);
#11229=EDGE_CURVE('',#8744,#8621,#4462,.T.);
#11230=EDGE_CURVE('',#8650,#8745,#4463,.T.);
#11231=EDGE_CURVE('',#8745,#8633,#4464,.T.);
#11232=EDGE_CURVE('',#8628,#8640,#4465,.T.);
#11233=EDGE_CURVE('',#8745,#8746,#4466,.T.);
#11234=EDGE_CURVE('',#8746,#8744,#4467,.T.);
#11235=EDGE_CURVE('',#8743,#8747,#4468,.T.);
#11236=EDGE_CURVE('',#8747,#8741,#4469,.T.);
#11237=EDGE_CURVE('',#8740,#8748,#4470,.T.);
#11238=EDGE_CURVE('',#8748,#8738,#4471,.T.);
#11239=EDGE_CURVE('',#8737,#8649,#4472,.T.);
#11240=EDGE_CURVE('',#8735,#8749,#4473,.T.);
#11241=EDGE_CURVE('',#8749,#8705,#4474,.T.);
#11242=EDGE_CURVE('',#8733,#8750,#4475,.T.);
#11243=EDGE_CURVE('',#8750,#8716,#4476,.T.);
#11244=EDGE_CURVE('',#8731,#8751,#4477,.T.);
#11245=EDGE_CURVE('',#8751,#8725,#4478,.T.);
#11246=EDGE_CURVE('',#8729,#8752,#4479,.T.);
#11247=EDGE_CURVE('',#8752,#8666,#4480,.T.);
#11248=EDGE_CURVE('',#8727,#8753,#4481,.T.);
#11249=EDGE_CURVE('',#8753,#8677,#4482,.T.);
#11250=EDGE_CURVE('',#8660,#8720,#5416,.T.);
#11251=EDGE_CURVE('',#8722,#8709,#5417,.T.);
#11252=EDGE_CURVE('',#8711,#8698,#5418,.T.);
#11253=EDGE_CURVE('',#8700,#8689,#5419,.T.);
#11254=EDGE_CURVE('',#8736,#8749,#3653,.T.);
#11255=EDGE_CURVE('',#8734,#8750,#3654,.T.);
#11256=EDGE_CURVE('',#8732,#8751,#3655,.T.);
#11257=EDGE_CURVE('',#8730,#8752,#3656,.T.);
#11258=EDGE_CURVE('',#8728,#8753,#3657,.T.);
#11259=EDGE_CURVE('',#8726,#8748,#3658,.T.);
#11260=EDGE_CURVE('',#8739,#8747,#3659,.T.);
#11261=EDGE_CURVE('',#8742,#8746,#3660,.T.);
#11262=EDGE_CURVE('',#8754,#8754,#3661,.T.);
#11263=EDGE_CURVE('',#8755,#8755,#3662,.T.);
#11264=EDGE_CURVE('',#8755,#8754,#5420,.T.);
#11265=EDGE_CURVE('',#8756,#8756,#3663,.T.);
#11266=EDGE_CURVE('',#8756,#8757,#5421,.T.);
#11267=EDGE_CURVE('',#8757,#8757,#3664,.T.);
#11268=EDGE_CURVE('',#8683,#8670,#5422,.T.);
#11269=EDGE_CURVE('',#8672,#8657,#5423,.T.);
#11270=EDGE_CURVE('',#8692,#8652,#5424,.T.);
#11271=EDGE_CURVE('',#8653,#8637,#5425,.T.);
#11272=EDGE_CURVE('',#8641,#8627,#5426,.T.);
#11273=EDGE_CURVE('',#8630,#8617,#5427,.T.);
#11274=EDGE_CURVE('',#8620,#8607,#5428,.T.);
#11275=EDGE_CURVE('',#8610,#8681,#5429,.T.);
#11276=EDGE_CURVE('',#8755,#8757,#5430,.T.);
#11277=EDGE_CURVE('',#8758,#8758,#3665,.T.);
#11278=EDGE_CURVE('',#8759,#8759,#3666,.T.);
#11279=EDGE_CURVE('',#8759,#8758,#5431,.T.);
#11280=EDGE_CURVE('',#8760,#8760,#3667,.T.);
#11281=EDGE_CURVE('',#8760,#8759,#5432,.T.);
#11282=EDGE_CURVE('',#8761,#8761,#3668,.T.);
#11283=EDGE_CURVE('',#8761,#8760,#5433,.T.);
#15659=ORIENTED_EDGE('',*,*,#11037,.T.);
#15660=ORIENTED_EDGE('',*,*,#11038,.T.);
#15661=ORIENTED_EDGE('',*,*,#11039,.T.);
#15662=ORIENTED_EDGE('',*,*,#11040,.T.);
#15663=ORIENTED_EDGE('',*,*,#11041,.T.);
#15664=ORIENTED_EDGE('',*,*,#11038,.F.);
#15665=ORIENTED_EDGE('',*,*,#11042,.F.);
#15666=ORIENTED_EDGE('',*,*,#11043,.F.);
#15667=ORIENTED_EDGE('',*,*,#11044,.F.);
#15668=ORIENTED_EDGE('',*,*,#11037,.F.);
#15669=ORIENTED_EDGE('',*,*,#11045,.F.);
#15670=ORIENTED_EDGE('',*,*,#11046,.T.);
#15671=ORIENTED_EDGE('',*,*,#11047,.T.);
#15672=ORIENTED_EDGE('',*,*,#11048,.T.);
#15673=ORIENTED_EDGE('',*,*,#11042,.T.);
#15674=ORIENTED_EDGE('',*,*,#11049,.T.);
#15675=ORIENTED_EDGE('',*,*,#11050,.T.);
#15676=ORIENTED_EDGE('',*,*,#11051,.T.);
#15677=ORIENTED_EDGE('',*,*,#11052,.T.);
#15678=ORIENTED_EDGE('',*,*,#11053,.T.);
#15679=ORIENTED_EDGE('',*,*,#11050,.F.);
#15680=ORIENTED_EDGE('',*,*,#11054,.F.);
#15681=ORIENTED_EDGE('',*,*,#11055,.F.);
#15682=ORIENTED_EDGE('',*,*,#11056,.F.);
#15683=ORIENTED_EDGE('',*,*,#11049,.F.);
#15684=ORIENTED_EDGE('',*,*,#11057,.F.);
#15685=ORIENTED_EDGE('',*,*,#11058,.T.);
#15686=ORIENTED_EDGE('',*,*,#11059,.T.);
#15687=ORIENTED_EDGE('',*,*,#11060,.T.);
#15688=ORIENTED_EDGE('',*,*,#11054,.T.);
#15689=ORIENTED_EDGE('',*,*,#11061,.T.);
#15690=ORIENTED_EDGE('',*,*,#11062,.T.);
#15691=ORIENTED_EDGE('',*,*,#11063,.T.);
#15692=ORIENTED_EDGE('',*,*,#11064,.T.);
#15693=ORIENTED_EDGE('',*,*,#11065,.T.);
#15694=ORIENTED_EDGE('',*,*,#11062,.F.);
#15695=ORIENTED_EDGE('',*,*,#11066,.F.);
#15696=ORIENTED_EDGE('',*,*,#11067,.F.);
#15697=ORIENTED_EDGE('',*,*,#11068,.F.);
#15698=ORIENTED_EDGE('',*,*,#11061,.F.);
#15699=ORIENTED_EDGE('',*,*,#11069,.F.);
#15700=ORIENTED_EDGE('',*,*,#11070,.T.);
#15701=ORIENTED_EDGE('',*,*,#11071,.T.);
#15702=ORIENTED_EDGE('',*,*,#11072,.T.);
#15703=ORIENTED_EDGE('',*,*,#11066,.T.);
#15704=ORIENTED_EDGE('',*,*,#11073,.T.);
#15705=ORIENTED_EDGE('',*,*,#11074,.T.);
#15706=ORIENTED_EDGE('',*,*,#11075,.T.);
#15707=ORIENTED_EDGE('',*,*,#11076,.T.);
#15708=ORIENTED_EDGE('',*,*,#11074,.F.);
#15709=ORIENTED_EDGE('',*,*,#11077,.T.);
#15710=ORIENTED_EDGE('',*,*,#11078,.T.);
#15711=ORIENTED_EDGE('',*,*,#11079,.F.);
#15712=ORIENTED_EDGE('',*,*,#11080,.F.);
#15713=ORIENTED_EDGE('',*,*,#11081,.F.);
#15714=ORIENTED_EDGE('',*,*,#11073,.F.);
#15715=ORIENTED_EDGE('',*,*,#11082,.F.);
#15716=ORIENTED_EDGE('',*,*,#11083,.F.);
#15717=ORIENTED_EDGE('',*,*,#11084,.F.);
#15718=ORIENTED_EDGE('',*,*,#11085,.F.);
#15719=ORIENTED_EDGE('',*,*,#11086,.F.);
#15720=ORIENTED_EDGE('',*,*,#11087,.F.);
#15721=ORIENTED_EDGE('',*,*,#11088,.F.);
#15722=ORIENTED_EDGE('',*,*,#11089,.F.);
#15723=ORIENTED_EDGE('',*,*,#11090,.F.);
#15724=ORIENTED_EDGE('',*,*,#11091,.F.);
#15725=ORIENTED_EDGE('',*,*,#11070,.F.);
#15726=ORIENTED_EDGE('',*,*,#11092,.F.);
#15727=ORIENTED_EDGE('',*,*,#11078,.F.);
#15728=ORIENTED_EDGE('',*,*,#11077,.F.);
#15729=ORIENTED_EDGE('',*,*,#11084,.T.);
#15730=ORIENTED_EDGE('',*,*,#11093,.T.);
#15731=ORIENTED_EDGE('',*,*,#11094,.T.);
#15732=ORIENTED_EDGE('',*,*,#11095,.T.);
#15733=ORIENTED_EDGE('',*,*,#11093,.F.);
#15734=ORIENTED_EDGE('',*,*,#11083,.T.);
#15735=ORIENTED_EDGE('',*,*,#11096,.F.);
#15736=ORIENTED_EDGE('',*,*,#11097,.F.);
#15737=ORIENTED_EDGE('',*,*,#11098,.T.);
#15738=ORIENTED_EDGE('',*,*,#11099,.T.);
#15739=ORIENTED_EDGE('',*,*,#11100,.T.);
#15740=ORIENTED_EDGE('',*,*,#11101,.T.);
#15741=ORIENTED_EDGE('',*,*,#11102,.T.);
#15742=ORIENTED_EDGE('',*,*,#11099,.F.);
#15743=ORIENTED_EDGE('',*,*,#11103,.F.);
#15744=ORIENTED_EDGE('',*,*,#11104,.F.);
#15745=ORIENTED_EDGE('',*,*,#11105,.F.);
#15746=ORIENTED_EDGE('',*,*,#11098,.F.);
#15747=ORIENTED_EDGE('',*,*,#11106,.T.);
#15748=ORIENTED_EDGE('',*,*,#11107,.T.);
#15749=ORIENTED_EDGE('',*,*,#11108,.T.);
#15750=ORIENTED_EDGE('',*,*,#11109,.F.);
#15751=ORIENTED_EDGE('',*,*,#11103,.T.);
#15752=ORIENTED_EDGE('',*,*,#11102,.F.);
#15753=ORIENTED_EDGE('',*,*,#11110,.T.);
#15754=ORIENTED_EDGE('',*,*,#11111,.T.);
#15755=ORIENTED_EDGE('',*,*,#11112,.F.);
#15756=ORIENTED_EDGE('',*,*,#11113,.T.);
#15757=ORIENTED_EDGE('',*,*,#11106,.F.);
#15758=ORIENTED_EDGE('',*,*,#11114,.T.);
#15759=ORIENTED_EDGE('',*,*,#11115,.T.);
#15760=ORIENTED_EDGE('',*,*,#11116,.T.);
#15761=ORIENTED_EDGE('',*,*,#11117,.T.);
#15762=ORIENTED_EDGE('',*,*,#11118,.T.);
#15763=ORIENTED_EDGE('',*,*,#11115,.F.);
#15764=ORIENTED_EDGE('',*,*,#11119,.F.);
#15765=ORIENTED_EDGE('',*,*,#11120,.F.);
#15766=ORIENTED_EDGE('',*,*,#11121,.F.);
#15767=ORIENTED_EDGE('',*,*,#11114,.F.);
#15768=ORIENTED_EDGE('',*,*,#11122,.T.);
#15769=ORIENTED_EDGE('',*,*,#11123,.T.);
#15770=ORIENTED_EDGE('',*,*,#11124,.T.);
#15771=ORIENTED_EDGE('',*,*,#11111,.F.);
#15772=ORIENTED_EDGE('',*,*,#11119,.T.);
#15773=ORIENTED_EDGE('',*,*,#11118,.F.);
#15774=ORIENTED_EDGE('',*,*,#11125,.T.);
#15775=ORIENTED_EDGE('',*,*,#11126,.T.);
#15776=ORIENTED_EDGE('',*,*,#11127,.F.);
#15777=ORIENTED_EDGE('',*,*,#11128,.T.);
#15778=ORIENTED_EDGE('',*,*,#11122,.F.);
#15779=ORIENTED_EDGE('',*,*,#11129,.T.);
#15780=ORIENTED_EDGE('',*,*,#11130,.T.);
#15781=ORIENTED_EDGE('',*,*,#11131,.T.);
#15782=ORIENTED_EDGE('',*,*,#11132,.T.);
#15783=ORIENTED_EDGE('',*,*,#11133,.T.);
#15784=ORIENTED_EDGE('',*,*,#11130,.F.);
#15785=ORIENTED_EDGE('',*,*,#11134,.F.);
#15786=ORIENTED_EDGE('',*,*,#11135,.F.);
#15787=ORIENTED_EDGE('',*,*,#11136,.F.);
#15788=ORIENTED_EDGE('',*,*,#11129,.F.);
#15789=ORIENTED_EDGE('',*,*,#11137,.F.);
#15790=ORIENTED_EDGE('',*,*,#11138,.T.);
#15791=ORIENTED_EDGE('',*,*,#11139,.T.);
#15792=ORIENTED_EDGE('',*,*,#11126,.F.);
#15793=ORIENTED_EDGE('',*,*,#11134,.T.);
#15794=ORIENTED_EDGE('',*,*,#11140,.T.);
#15795=ORIENTED_EDGE('',*,*,#11141,.T.);
#15796=ORIENTED_EDGE('',*,*,#11142,.T.);
#15797=ORIENTED_EDGE('',*,*,#11143,.T.);
#15798=ORIENTED_EDGE('',*,*,#11144,.T.);
#15799=ORIENTED_EDGE('',*,*,#11141,.F.);
#15800=ORIENTED_EDGE('',*,*,#11145,.F.);
#15801=ORIENTED_EDGE('',*,*,#11146,.F.);
#15802=ORIENTED_EDGE('',*,*,#11147,.F.);
#15803=ORIENTED_EDGE('',*,*,#11140,.F.);
#15804=ORIENTED_EDGE('',*,*,#11148,.T.);
#15805=ORIENTED_EDGE('',*,*,#11087,.T.);
#15806=ORIENTED_EDGE('',*,*,#11149,.T.);
#15807=ORIENTED_EDGE('',*,*,#11145,.T.);
#15808=ORIENTED_EDGE('',*,*,#11144,.F.);
#15809=ORIENTED_EDGE('',*,*,#11150,.T.);
#15810=ORIENTED_EDGE('',*,*,#11151,.T.);
#15811=ORIENTED_EDGE('',*,*,#11152,.F.);
#15812=ORIENTED_EDGE('',*,*,#11088,.T.);
#15813=ORIENTED_EDGE('',*,*,#11148,.F.);
#15814=ORIENTED_EDGE('',*,*,#11153,.T.);
#15815=ORIENTED_EDGE('',*,*,#11154,.T.);
#15816=ORIENTED_EDGE('',*,*,#11155,.T.);
#15817=ORIENTED_EDGE('',*,*,#11156,.T.);
#15818=ORIENTED_EDGE('',*,*,#11157,.T.);
#15819=ORIENTED_EDGE('',*,*,#11154,.F.);
#15820=ORIENTED_EDGE('',*,*,#11158,.F.);
#15821=ORIENTED_EDGE('',*,*,#11159,.F.);
#15822=ORIENTED_EDGE('',*,*,#11160,.F.);
#15823=ORIENTED_EDGE('',*,*,#11153,.F.);
#15824=ORIENTED_EDGE('',*,*,#11161,.T.);
#15825=ORIENTED_EDGE('',*,*,#11162,.T.);
#15826=ORIENTED_EDGE('',*,*,#11163,.T.);
#15827=ORIENTED_EDGE('',*,*,#11151,.F.);
#15828=ORIENTED_EDGE('',*,*,#11158,.T.);
#15829=ORIENTED_EDGE('',*,*,#11157,.F.);
#15830=ORIENTED_EDGE('',*,*,#11164,.T.);
#15831=ORIENTED_EDGE('',*,*,#11165,.T.);
#15832=ORIENTED_EDGE('',*,*,#11166,.F.);
#15833=ORIENTED_EDGE('',*,*,#11167,.T.);
#15834=ORIENTED_EDGE('',*,*,#11161,.F.);
#15835=ORIENTED_EDGE('',*,*,#11168,.T.);
#15836=ORIENTED_EDGE('',*,*,#11169,.T.);
#15837=ORIENTED_EDGE('',*,*,#11170,.T.);
#15838=ORIENTED_EDGE('',*,*,#11171,.T.);
#15839=ORIENTED_EDGE('',*,*,#11172,.T.);
#15840=ORIENTED_EDGE('',*,*,#11169,.F.);
#15841=ORIENTED_EDGE('',*,*,#11173,.F.);
#15842=ORIENTED_EDGE('',*,*,#11174,.F.);
#15843=ORIENTED_EDGE('',*,*,#11175,.F.);
#15844=ORIENTED_EDGE('',*,*,#11168,.F.);
#15845=ORIENTED_EDGE('',*,*,#11176,.T.);
#15846=ORIENTED_EDGE('',*,*,#11177,.T.);
#15847=ORIENTED_EDGE('',*,*,#11178,.T.);
#15848=ORIENTED_EDGE('',*,*,#11165,.F.);
#15849=ORIENTED_EDGE('',*,*,#11173,.T.);
#15850=ORIENTED_EDGE('',*,*,#11172,.F.);
#15851=ORIENTED_EDGE('',*,*,#11179,.T.);
#15852=ORIENTED_EDGE('',*,*,#11180,.T.);
#15853=ORIENTED_EDGE('',*,*,#11181,.F.);
#15854=ORIENTED_EDGE('',*,*,#11182,.T.);
#15855=ORIENTED_EDGE('',*,*,#11176,.F.);
#15856=ORIENTED_EDGE('',*,*,#11183,.T.);
#15857=ORIENTED_EDGE('',*,*,#11184,.T.);
#15858=ORIENTED_EDGE('',*,*,#11185,.T.);
#15859=ORIENTED_EDGE('',*,*,#11186,.T.);
#15860=ORIENTED_EDGE('',*,*,#11187,.T.);
#15861=ORIENTED_EDGE('',*,*,#11184,.F.);
#15862=ORIENTED_EDGE('',*,*,#11188,.F.);
#15863=ORIENTED_EDGE('',*,*,#11189,.F.);
#15864=ORIENTED_EDGE('',*,*,#11190,.F.);
#15865=ORIENTED_EDGE('',*,*,#11183,.F.);
#15866=ORIENTED_EDGE('',*,*,#11191,.T.);
#15867=ORIENTED_EDGE('',*,*,#11192,.T.);
#15868=ORIENTED_EDGE('',*,*,#11193,.T.);
#15869=ORIENTED_EDGE('',*,*,#11180,.F.);
#15870=ORIENTED_EDGE('',*,*,#11188,.T.);
#15871=ORIENTED_EDGE('',*,*,#11187,.F.);
#15872=ORIENTED_EDGE('',*,*,#11194,.T.);
#15873=ORIENTED_EDGE('',*,*,#11109,.T.);
#15874=ORIENTED_EDGE('',*,*,#11195,.F.);
#15875=ORIENTED_EDGE('',*,*,#11196,.T.);
#15876=ORIENTED_EDGE('',*,*,#11191,.F.);
#15877=ORIENTED_EDGE('',*,*,#11139,.F.);
#15878=ORIENTED_EDGE('',*,*,#11197,.T.);
#15879=ORIENTED_EDGE('',*,*,#11198,.T.);
#15880=ORIENTED_EDGE('',*,*,#11199,.F.);
#15881=ORIENTED_EDGE('',*,*,#11124,.F.);
#15882=ORIENTED_EDGE('',*,*,#11200,.T.);
#15883=ORIENTED_EDGE('',*,*,#11201,.T.);
#15884=ORIENTED_EDGE('',*,*,#11202,.F.);
#15885=ORIENTED_EDGE('',*,*,#11108,.F.);
#15886=ORIENTED_EDGE('',*,*,#11203,.T.);
#15887=ORIENTED_EDGE('',*,*,#11204,.T.);
#15888=ORIENTED_EDGE('',*,*,#11205,.F.);
#15889=ORIENTED_EDGE('',*,*,#11193,.F.);
#15890=ORIENTED_EDGE('',*,*,#11206,.T.);
#15891=ORIENTED_EDGE('',*,*,#11207,.T.);
#15892=ORIENTED_EDGE('',*,*,#11208,.F.);
#15893=ORIENTED_EDGE('',*,*,#11178,.F.);
#15894=ORIENTED_EDGE('',*,*,#11209,.T.);
#15895=ORIENTED_EDGE('',*,*,#11210,.T.);
#15896=ORIENTED_EDGE('',*,*,#11211,.F.);
#15897=ORIENTED_EDGE('',*,*,#11163,.F.);
#15898=ORIENTED_EDGE('',*,*,#11212,.T.);
#15899=ORIENTED_EDGE('',*,*,#11213,.T.);
#15900=ORIENTED_EDGE('',*,*,#11214,.F.);
#15901=ORIENTED_EDGE('',*,*,#11133,.F.);
#15902=ORIENTED_EDGE('',*,*,#11215,.T.);
#15903=ORIENTED_EDGE('',*,*,#11048,.F.);
#15904=ORIENTED_EDGE('',*,*,#11216,.F.);
#15905=ORIENTED_EDGE('',*,*,#11217,.T.);
#15906=ORIENTED_EDGE('',*,*,#11137,.T.);
#15907=ORIENTED_EDGE('',*,*,#11047,.F.);
#15908=ORIENTED_EDGE('',*,*,#11218,.T.);
#15909=ORIENTED_EDGE('',*,*,#11219,.T.);
#15910=ORIENTED_EDGE('',*,*,#11220,.T.);
#15911=ORIENTED_EDGE('',*,*,#11041,.F.);
#15912=ORIENTED_EDGE('',*,*,#11221,.T.);
#15913=ORIENTED_EDGE('',*,*,#11060,.F.);
#15914=ORIENTED_EDGE('',*,*,#11222,.F.);
#15915=ORIENTED_EDGE('',*,*,#11223,.T.);
#15916=ORIENTED_EDGE('',*,*,#11045,.T.);
#15917=ORIENTED_EDGE('',*,*,#11059,.F.);
#15918=ORIENTED_EDGE('',*,*,#11224,.T.);
#15919=ORIENTED_EDGE('',*,*,#11225,.T.);
#15920=ORIENTED_EDGE('',*,*,#11226,.T.);
#15921=ORIENTED_EDGE('',*,*,#11053,.F.);
#15922=ORIENTED_EDGE('',*,*,#11227,.T.);
#15923=ORIENTED_EDGE('',*,*,#11072,.F.);
#15924=ORIENTED_EDGE('',*,*,#11228,.F.);
#15925=ORIENTED_EDGE('',*,*,#11229,.T.);
#15926=ORIENTED_EDGE('',*,*,#11057,.T.);
#15927=ORIENTED_EDGE('',*,*,#11071,.F.);
#15928=ORIENTED_EDGE('',*,*,#11091,.T.);
#15929=ORIENTED_EDGE('',*,*,#11230,.T.);
#15930=ORIENTED_EDGE('',*,*,#11231,.T.);
#15931=ORIENTED_EDGE('',*,*,#11065,.F.);
#15932=ORIENTED_EDGE('',*,*,#11232,.T.);
#15933=ORIENTED_EDGE('',*,*,#11079,.T.);
#15934=ORIENTED_EDGE('',*,*,#11092,.T.);
#15935=ORIENTED_EDGE('',*,*,#11069,.T.);
#15936=ORIENTED_EDGE('',*,*,#11228,.T.);
#15937=ORIENTED_EDGE('',*,*,#11231,.F.);
#15938=ORIENTED_EDGE('',*,*,#11233,.T.);
#15939=ORIENTED_EDGE('',*,*,#11234,.T.);
#15940=ORIENTED_EDGE('',*,*,#11222,.T.);
#15941=ORIENTED_EDGE('',*,*,#11226,.F.);
#15942=ORIENTED_EDGE('',*,*,#11235,.T.);
#15943=ORIENTED_EDGE('',*,*,#11236,.T.);
#15944=ORIENTED_EDGE('',*,*,#11216,.T.);
#15945=ORIENTED_EDGE('',*,*,#11220,.F.);
#15946=ORIENTED_EDGE('',*,*,#11237,.T.);
#15947=ORIENTED_EDGE('',*,*,#11238,.T.);
#15948=ORIENTED_EDGE('',*,*,#11152,.T.);
#15949=ORIENTED_EDGE('',*,*,#11214,.T.);
#15950=ORIENTED_EDGE('',*,*,#11239,.T.);
#15951=ORIENTED_EDGE('',*,*,#11089,.T.);
#15952=ORIENTED_EDGE('',*,*,#11166,.T.);
#15953=ORIENTED_EDGE('',*,*,#11211,.T.);
#15954=ORIENTED_EDGE('',*,*,#11240,.T.);
#15955=ORIENTED_EDGE('',*,*,#11241,.T.);
#15956=ORIENTED_EDGE('',*,*,#11181,.T.);
#15957=ORIENTED_EDGE('',*,*,#11208,.T.);
#15958=ORIENTED_EDGE('',*,*,#11242,.T.);
#15959=ORIENTED_EDGE('',*,*,#11243,.T.);
#15960=ORIENTED_EDGE('',*,*,#11195,.T.);
#15961=ORIENTED_EDGE('',*,*,#11205,.T.);
#15962=ORIENTED_EDGE('',*,*,#11244,.T.);
#15963=ORIENTED_EDGE('',*,*,#11245,.T.);
#15964=ORIENTED_EDGE('',*,*,#11112,.T.);
#15965=ORIENTED_EDGE('',*,*,#11202,.T.);
#15966=ORIENTED_EDGE('',*,*,#11246,.T.);
#15967=ORIENTED_EDGE('',*,*,#11247,.T.);
#15968=ORIENTED_EDGE('',*,*,#11127,.T.);
#15969=ORIENTED_EDGE('',*,*,#11199,.T.);
#15970=ORIENTED_EDGE('',*,*,#11248,.T.);
#15971=ORIENTED_EDGE('',*,*,#11249,.T.);
#15972=ORIENTED_EDGE('',*,*,#11186,.F.);
#15973=ORIENTED_EDGE('',*,*,#11250,.F.);
#15974=ORIENTED_EDGE('',*,*,#11104,.T.);
#15975=ORIENTED_EDGE('',*,*,#11194,.F.);
#15976=ORIENTED_EDGE('',*,*,#11171,.F.);
#15977=ORIENTED_EDGE('',*,*,#11251,.F.);
#15978=ORIENTED_EDGE('',*,*,#11189,.T.);
#15979=ORIENTED_EDGE('',*,*,#11179,.F.);
#15980=ORIENTED_EDGE('',*,*,#11156,.F.);
#15981=ORIENTED_EDGE('',*,*,#11252,.F.);
#15982=ORIENTED_EDGE('',*,*,#11174,.T.);
#15983=ORIENTED_EDGE('',*,*,#11164,.F.);
#15984=ORIENTED_EDGE('',*,*,#11143,.F.);
#15985=ORIENTED_EDGE('',*,*,#11253,.F.);
#15986=ORIENTED_EDGE('',*,*,#11159,.T.);
#15987=ORIENTED_EDGE('',*,*,#11150,.F.);
#15988=ORIENTED_EDGE('',*,*,#11239,.F.);
#15989=ORIENTED_EDGE('',*,*,#11213,.F.);
#15990=ORIENTED_EDGE('',*,*,#11254,.T.);
#15991=ORIENTED_EDGE('',*,*,#11240,.F.);
#15992=ORIENTED_EDGE('',*,*,#11210,.F.);
#15993=ORIENTED_EDGE('',*,*,#11255,.T.);
#15994=ORIENTED_EDGE('',*,*,#11242,.F.);
#15995=ORIENTED_EDGE('',*,*,#11207,.F.);
#15996=ORIENTED_EDGE('',*,*,#11256,.T.);
#15997=ORIENTED_EDGE('',*,*,#11244,.F.);
#15998=ORIENTED_EDGE('',*,*,#11204,.F.);
#15999=ORIENTED_EDGE('',*,*,#11257,.T.);
#16000=ORIENTED_EDGE('',*,*,#11246,.F.);
#16001=ORIENTED_EDGE('',*,*,#11201,.F.);
#16002=ORIENTED_EDGE('',*,*,#11258,.T.);
#16003=ORIENTED_EDGE('',*,*,#11248,.F.);
#16004=ORIENTED_EDGE('',*,*,#11198,.F.);
#16005=ORIENTED_EDGE('',*,*,#11259,.T.);
#16006=ORIENTED_EDGE('',*,*,#11237,.F.);
#16007=ORIENTED_EDGE('',*,*,#11219,.F.);
#16008=ORIENTED_EDGE('',*,*,#11260,.T.);
#16009=ORIENTED_EDGE('',*,*,#11235,.F.);
#16010=ORIENTED_EDGE('',*,*,#11225,.F.);
#16011=ORIENTED_EDGE('',*,*,#11261,.T.);
#16012=ORIENTED_EDGE('',*,*,#11233,.F.);
#16013=ORIENTED_EDGE('',*,*,#11230,.F.);
#16014=ORIENTED_EDGE('',*,*,#11090,.T.);
#16015=ORIENTED_EDGE('',*,*,#11262,.T.);
#16016=ORIENTED_EDGE('',*,*,#11162,.F.);
#16017=ORIENTED_EDGE('',*,*,#11167,.F.);
#16018=ORIENTED_EDGE('',*,*,#11241,.F.);
#16019=ORIENTED_EDGE('',*,*,#11254,.F.);
#16020=ORIENTED_EDGE('',*,*,#11212,.F.);
#16021=ORIENTED_EDGE('',*,*,#11177,.F.);
#16022=ORIENTED_EDGE('',*,*,#11182,.F.);
#16023=ORIENTED_EDGE('',*,*,#11243,.F.);
#16024=ORIENTED_EDGE('',*,*,#11255,.F.);
#16025=ORIENTED_EDGE('',*,*,#11209,.F.);
#16026=ORIENTED_EDGE('',*,*,#11192,.F.);
#16027=ORIENTED_EDGE('',*,*,#11196,.F.);
#16028=ORIENTED_EDGE('',*,*,#11245,.F.);
#16029=ORIENTED_EDGE('',*,*,#11256,.F.);
#16030=ORIENTED_EDGE('',*,*,#11206,.F.);
#16031=ORIENTED_EDGE('',*,*,#11107,.F.);
#16032=ORIENTED_EDGE('',*,*,#11113,.F.);
#16033=ORIENTED_EDGE('',*,*,#11247,.F.);
#16034=ORIENTED_EDGE('',*,*,#11257,.F.);
#16035=ORIENTED_EDGE('',*,*,#11203,.F.);
#16036=ORIENTED_EDGE('',*,*,#11249,.F.);
#16037=ORIENTED_EDGE('',*,*,#11258,.F.);
#16038=ORIENTED_EDGE('',*,*,#11200,.F.);
#16039=ORIENTED_EDGE('',*,*,#11123,.F.);
#16040=ORIENTED_EDGE('',*,*,#11128,.F.);
#16041=ORIENTED_EDGE('',*,*,#11238,.F.);
#16042=ORIENTED_EDGE('',*,*,#11259,.F.);
#16043=ORIENTED_EDGE('',*,*,#11197,.F.);
#16044=ORIENTED_EDGE('',*,*,#11138,.F.);
#16045=ORIENTED_EDGE('',*,*,#11217,.F.);
#16046=ORIENTED_EDGE('',*,*,#11236,.F.);
#16047=ORIENTED_EDGE('',*,*,#11260,.F.);
#16048=ORIENTED_EDGE('',*,*,#11218,.F.);
#16049=ORIENTED_EDGE('',*,*,#11046,.F.);
#16050=ORIENTED_EDGE('',*,*,#11223,.F.);
#16051=ORIENTED_EDGE('',*,*,#11234,.F.);
#16052=ORIENTED_EDGE('',*,*,#11261,.F.);
#16053=ORIENTED_EDGE('',*,*,#11224,.F.);
#16054=ORIENTED_EDGE('',*,*,#11058,.F.);
#16055=ORIENTED_EDGE('',*,*,#11229,.F.);
#16056=ORIENTED_EDGE('',*,*,#11263,.F.);
#16057=ORIENTED_EDGE('',*,*,#11264,.T.);
#16058=ORIENTED_EDGE('',*,*,#11262,.F.);
#16059=ORIENTED_EDGE('',*,*,#11264,.F.);
#16060=ORIENTED_EDGE('',*,*,#11265,.F.);
#16061=ORIENTED_EDGE('',*,*,#11266,.T.);
#16062=ORIENTED_EDGE('',*,*,#11267,.F.);
#16063=ORIENTED_EDGE('',*,*,#11266,.F.);
#16064=ORIENTED_EDGE('',*,*,#11117,.F.);
#16065=ORIENTED_EDGE('',*,*,#11268,.F.);
#16066=ORIENTED_EDGE('',*,*,#11135,.T.);
#16067=ORIENTED_EDGE('',*,*,#11125,.F.);
#16068=ORIENTED_EDGE('',*,*,#11101,.F.);
#16069=ORIENTED_EDGE('',*,*,#11269,.F.);
#16070=ORIENTED_EDGE('',*,*,#11120,.T.);
#16071=ORIENTED_EDGE('',*,*,#11110,.F.);
#16072=ORIENTED_EDGE('',*,*,#11095,.F.);
#16073=ORIENTED_EDGE('',*,*,#11270,.F.);
#16074=ORIENTED_EDGE('',*,*,#11146,.T.);
#16075=ORIENTED_EDGE('',*,*,#11149,.F.);
#16076=ORIENTED_EDGE('',*,*,#11086,.T.);
#16077=ORIENTED_EDGE('',*,*,#11085,.T.);
#16078=ORIENTED_EDGE('',*,*,#11076,.F.);
#16079=ORIENTED_EDGE('',*,*,#11271,.F.);
#16080=ORIENTED_EDGE('',*,*,#11096,.T.);
#16081=ORIENTED_EDGE('',*,*,#11082,.T.);
#16082=ORIENTED_EDGE('',*,*,#11064,.F.);
#16083=ORIENTED_EDGE('',*,*,#11272,.F.);
#16084=ORIENTED_EDGE('',*,*,#11080,.T.);
#16085=ORIENTED_EDGE('',*,*,#11232,.F.);
#16086=ORIENTED_EDGE('',*,*,#11052,.F.);
#16087=ORIENTED_EDGE('',*,*,#11273,.F.);
#16088=ORIENTED_EDGE('',*,*,#11067,.T.);
#16089=ORIENTED_EDGE('',*,*,#11227,.F.);
#16090=ORIENTED_EDGE('',*,*,#11040,.F.);
#16091=ORIENTED_EDGE('',*,*,#11274,.F.);
#16092=ORIENTED_EDGE('',*,*,#11055,.T.);
#16093=ORIENTED_EDGE('',*,*,#11221,.F.);
#16094=ORIENTED_EDGE('',*,*,#11132,.F.);
#16095=ORIENTED_EDGE('',*,*,#11275,.F.);
#16096=ORIENTED_EDGE('',*,*,#11043,.T.);
#16097=ORIENTED_EDGE('',*,*,#11215,.F.);
#16098=ORIENTED_EDGE('',*,*,#11263,.T.);
#16099=ORIENTED_EDGE('',*,*,#11276,.T.);
#16100=ORIENTED_EDGE('',*,*,#11267,.T.);
#16101=ORIENTED_EDGE('',*,*,#11276,.F.);
#16102=ORIENTED_EDGE('',*,*,#11277,.F.);
#16103=ORIENTED_EDGE('',*,*,#11265,.T.);
#16104=ORIENTED_EDGE('',*,*,#11278,.F.);
#16105=ORIENTED_EDGE('',*,*,#11279,.T.);
#16106=ORIENTED_EDGE('',*,*,#11277,.T.);
#16107=ORIENTED_EDGE('',*,*,#11279,.F.);
#16108=ORIENTED_EDGE('',*,*,#11280,.F.);
#16109=ORIENTED_EDGE('',*,*,#11281,.T.);
#16110=ORIENTED_EDGE('',*,*,#11278,.T.);
#16111=ORIENTED_EDGE('',*,*,#11281,.F.);
#16112=ORIENTED_EDGE('',*,*,#11282,.F.);
#16113=ORIENTED_EDGE('',*,*,#11283,.T.);
#16114=ORIENTED_EDGE('',*,*,#11280,.T.);
#16115=ORIENTED_EDGE('',*,*,#11283,.F.);
#16116=ORIENTED_EDGE('',*,*,#11282,.T.);
#16117=ORIENTED_EDGE('',*,*,#11268,.T.);
#16118=ORIENTED_EDGE('',*,*,#11116,.F.);
#16119=ORIENTED_EDGE('',*,*,#11121,.T.);
#16120=ORIENTED_EDGE('',*,*,#11269,.T.);
#16121=ORIENTED_EDGE('',*,*,#11100,.F.);
#16122=ORIENTED_EDGE('',*,*,#11105,.T.);
#16123=ORIENTED_EDGE('',*,*,#11250,.T.);
#16124=ORIENTED_EDGE('',*,*,#11185,.F.);
#16125=ORIENTED_EDGE('',*,*,#11190,.T.);
#16126=ORIENTED_EDGE('',*,*,#11251,.T.);
#16127=ORIENTED_EDGE('',*,*,#11170,.F.);
#16128=ORIENTED_EDGE('',*,*,#11175,.T.);
#16129=ORIENTED_EDGE('',*,*,#11252,.T.);
#16130=ORIENTED_EDGE('',*,*,#11155,.F.);
#16131=ORIENTED_EDGE('',*,*,#11160,.T.);
#16132=ORIENTED_EDGE('',*,*,#11253,.T.);
#16133=ORIENTED_EDGE('',*,*,#11142,.F.);
#16134=ORIENTED_EDGE('',*,*,#11147,.T.);
#16135=ORIENTED_EDGE('',*,*,#11270,.T.);
#16136=ORIENTED_EDGE('',*,*,#11094,.F.);
#16137=ORIENTED_EDGE('',*,*,#11097,.T.);
#16138=ORIENTED_EDGE('',*,*,#11271,.T.);
#16139=ORIENTED_EDGE('',*,*,#11075,.F.);
#16140=ORIENTED_EDGE('',*,*,#11081,.T.);
#16141=ORIENTED_EDGE('',*,*,#11272,.T.);
#16142=ORIENTED_EDGE('',*,*,#11063,.F.);
#16143=ORIENTED_EDGE('',*,*,#11068,.T.);
#16144=ORIENTED_EDGE('',*,*,#11273,.T.);
#16145=ORIENTED_EDGE('',*,*,#11051,.F.);
#16146=ORIENTED_EDGE('',*,*,#11056,.T.);
#16147=ORIENTED_EDGE('',*,*,#11274,.T.);
#16148=ORIENTED_EDGE('',*,*,#11039,.F.);
#16149=ORIENTED_EDGE('',*,*,#11044,.T.);
#16150=ORIENTED_EDGE('',*,*,#11275,.T.);
#16151=ORIENTED_EDGE('',*,*,#11131,.F.);
#16152=ORIENTED_EDGE('',*,*,#11136,.T.);
#17317=CYLINDRICAL_SURFACE('',#19430,3.55);
#17318=CYLINDRICAL_SURFACE('',#19435,6.5);
#18019=ADVANCED_FACE('',(#1991),#624,.T.);
#18020=ADVANCED_FACE('',(#1992),#625,.T.);
#18021=ADVANCED_FACE('',(#1993),#159,.T.);
#18022=ADVANCED_FACE('',(#1994),#626,.T.);
#18023=ADVANCED_FACE('',(#1995),#627,.T.);
#18024=ADVANCED_FACE('',(#1996),#160,.T.);
#18025=ADVANCED_FACE('',(#1997),#628,.T.);
#18026=ADVANCED_FACE('',(#1998),#629,.T.);
#18027=ADVANCED_FACE('',(#1999),#161,.T.);
#18028=ADVANCED_FACE('',(#2000),#630,.T.);
#18029=ADVANCED_FACE('',(#2001),#631,.T.);
#18030=ADVANCED_FACE('',(#2002),#955,.T.);
#18031=ADVANCED_FACE('',(#2003),#632,.T.);
#18032=ADVANCED_FACE('',(#2004),#633,.T.);
#18033=ADVANCED_FACE('',(#2005),#634,.T.);
#18034=ADVANCED_FACE('',(#2006),#635,.T.);
#18035=ADVANCED_FACE('',(#2007),#162,.T.);
#18036=ADVANCED_FACE('',(#2008),#163,.T.);
#18037=ADVANCED_FACE('',(#2009),#636,.T.);
#18038=ADVANCED_FACE('',(#2010),#637,.T.);
#18039=ADVANCED_FACE('',(#2011),#164,.T.);
#18040=ADVANCED_FACE('',(#2012),#165,.T.);
#18041=ADVANCED_FACE('',(#2013),#638,.T.);
#18042=ADVANCED_FACE('',(#2014),#639,.T.);
#18043=ADVANCED_FACE('',(#2015),#166,.T.);
#18044=ADVANCED_FACE('',(#2016),#640,.T.);
#18045=ADVANCED_FACE('',(#2017),#641,.T.);
#18046=ADVANCED_FACE('',(#2018),#167,.T.);
#18047=ADVANCED_FACE('',(#2019),#168,.T.);
#18048=ADVANCED_FACE('',(#2020),#642,.T.);
#18049=ADVANCED_FACE('',(#2021),#643,.T.);
#18050=ADVANCED_FACE('',(#2022),#169,.T.);
#18051=ADVANCED_FACE('',(#2023),#170,.T.);
#18052=ADVANCED_FACE('',(#2024),#644,.T.);
#18053=ADVANCED_FACE('',(#2025),#645,.T.);
#18054=ADVANCED_FACE('',(#2026),#171,.T.);
#18055=ADVANCED_FACE('',(#2027),#172,.T.);
#18056=ADVANCED_FACE('',(#2028),#646,.T.);
#18057=ADVANCED_FACE('',(#2029),#647,.T.);
#18058=ADVANCED_FACE('',(#2030),#173,.T.);
#18059=ADVANCED_FACE('',(#2031),#174,.T.);
#18060=ADVANCED_FACE('',(#2032),#175,.T.);
#18061=ADVANCED_FACE('',(#2033),#176,.T.);
#18062=ADVANCED_FACE('',(#2034),#177,.T.);
#18063=ADVANCED_FACE('',(#2035),#178,.T.);
#18064=ADVANCED_FACE('',(#2036),#179,.T.);
#18065=ADVANCED_FACE('',(#2037),#180,.T.);
#18066=ADVANCED_FACE('',(#2038),#181,.T.);
#18067=ADVANCED_FACE('',(#2039),#182,.T.);
#18068=ADVANCED_FACE('',(#2040),#183,.T.);
#18069=ADVANCED_FACE('',(#2041),#184,.T.);
#18070=ADVANCED_FACE('',(#2042),#185,.T.);
#18071=ADVANCED_FACE('',(#2043),#186,.T.);
#18072=ADVANCED_FACE('',(#2044),#187,.T.);
#18073=ADVANCED_FACE('',(#2045),#188,.T.);
#18074=ADVANCED_FACE('',(#2046),#189,.T.);
#18075=ADVANCED_FACE('',(#2047),#190,.T.);
#18076=ADVANCED_FACE('',(#2048),#191,.T.);
#18077=ADVANCED_FACE('',(#2049),#192,.T.);
#18078=ADVANCED_FACE('',(#2050),#193,.T.);
#18079=ADVANCED_FACE('',(#2051),#194,.T.);
#18080=ADVANCED_FACE('',(#2052),#195,.T.);
#18081=ADVANCED_FACE('',(#2053),#196,.T.);
#18082=ADVANCED_FACE('',(#2054),#648,.T.);
#18083=ADVANCED_FACE('',(#2055),#649,.T.);
#18084=ADVANCED_FACE('',(#2056),#650,.T.);
#18085=ADVANCED_FACE('',(#2057),#651,.T.);
#18086=ADVANCED_FACE('',(#2058,#243),#652,.T.);
#18087=ADVANCED_FACE('',(#2059),#956,.T.);
#18088=ADVANCED_FACE('',(#2060),#957,.T.);
#18089=ADVANCED_FACE('',(#2061),#958,.T.);
#18090=ADVANCED_FACE('',(#2062),#959,.T.);
#18091=ADVANCED_FACE('',(#2063),#960,.T.);
#18092=ADVANCED_FACE('',(#2064),#961,.T.);
#18093=ADVANCED_FACE('',(#2065),#962,.T.);
#18094=ADVANCED_FACE('',(#2066),#963,.T.);
#18095=ADVANCED_FACE('',(#2067),#964,.F.);
#18096=ADVANCED_FACE('',(#2068),#965,.F.);
#18097=ADVANCED_FACE('',(#2069),#653,.T.);
#18098=ADVANCED_FACE('',(#2070),#654,.T.);
#18099=ADVANCED_FACE('',(#2071),#655,.T.);
#18100=ADVANCED_FACE('',(#2072),#656,.T.);
#18101=ADVANCED_FACE('',(#2073),#657,.T.);
#18102=ADVANCED_FACE('',(#2074),#658,.T.);
#18103=ADVANCED_FACE('',(#2075),#659,.T.);
#18104=ADVANCED_FACE('',(#2076),#660,.T.);
#18105=ADVANCED_FACE('',(#2077),#17317,.F.);
#18106=ADVANCED_FACE('',(#2078,#244),#661,.T.);
#18107=ADVANCED_FACE('',(#2079),#966,.T.);
#18108=ADVANCED_FACE('',(#2080),#17318,.T.);
#18109=ADVANCED_FACE('',(#2081),#967,.T.);
#18110=ADVANCED_FACE('',(#2082,#245),#662,.T.);
#18304=CLOSED_SHELL('',(#18019,#18020,#18021,#18022,#18023,#18024,#18025,
#18026,#18027,#18028,#18029,#18030,#18031,#18032,#18033,#18034,#18035,#18036,
#18037,#18038,#18039,#18040,#18041,#18042,#18043,#18044,#18045,#18046,#18047,
#18048,#18049,#18050,#18051,#18052,#18053,#18054,#18055,#18056,#18057,#18058,
#18059,#18060,#18061,#18062,#18063,#18064,#18065,#18066,#18067,#18068,#18069,
#18070,#18071,#18072,#18073,#18074,#18075,#18076,#18077,#18078,#18079,#18080,
#18081,#18082,#18083,#18084,#18085,#18086,#18087,#18088,#18089,#18090,#18091,
#18092,#18093,#18094,#18095,#18096,#18097,#18098,#18099,#18100,#18101,#18102,
#18103,#18104,#18105,#18106,#18107,#18108,#18109,#18110));
#19368=AXIS2_PLACEMENT_3D('',#57382,#22434,#22435);
#19369=AXIS2_PLACEMENT_3D('',#57383,#22436,#22437);
#19370=AXIS2_PLACEMENT_3D('',#57405,#22441,#22442);
#19371=AXIS2_PLACEMENT_3D('',#57449,#22445,#22446);
#19372=AXIS2_PLACEMENT_3D('',#57471,#22450,#22451);
#19373=AXIS2_PLACEMENT_3D('',#57515,#22454,#22455);
#19374=AXIS2_PLACEMENT_3D('',#57537,#22459,#22460);
#19375=AXIS2_PLACEMENT_3D('',#57581,#22463,#22464);
#19376=AXIS2_PLACEMENT_3D('',#57592,#22468,#22469);
#19377=AXIS2_PLACEMENT_3D('',#57611,#22472,#22473);
#19378=AXIS2_PLACEMENT_3D('',#57648,#22474,#22475);
#19379=AXIS2_PLACEMENT_3D('',#57657,#22476,#22477);
#19380=AXIS2_PLACEMENT_3D('',#57663,#22481,#22482);
#19381=AXIS2_PLACEMENT_3D('',#57667,#22485,#22486);
#19382=AXIS2_PLACEMENT_3D('',#57689,#22490,#22491);
#19383=AXIS2_PLACEMENT_3D('',#57768,#22494,#22495);
#19384=AXIS2_PLACEMENT_3D('',#57790,#22499,#22500);
#19385=AXIS2_PLACEMENT_3D('',#57863,#22503,#22504);
#19386=AXIS2_PLACEMENT_3D('',#57885,#22508,#22509);
#19387=AXIS2_PLACEMENT_3D('',#57923,#22512,#22513);
#19388=AXIS2_PLACEMENT_3D('',#57945,#22517,#22518);
#19389=AXIS2_PLACEMENT_3D('',#58010,#22521,#22522);
#19390=AXIS2_PLACEMENT_3D('',#58032,#22526,#22527);
#19391=AXIS2_PLACEMENT_3D('',#58105,#22530,#22531);
#19392=AXIS2_PLACEMENT_3D('',#58127,#22535,#22536);
#19393=AXIS2_PLACEMENT_3D('',#58200,#22539,#22540);
#19394=AXIS2_PLACEMENT_3D('',#58222,#22544,#22545);
#19395=AXIS2_PLACEMENT_3D('',#58908,#22548,#22549);
#19396=AXIS2_PLACEMENT_3D('',#58910,#22551,#22552);
#19397=AXIS2_PLACEMENT_3D('',#58912,#22554,#22555);
#19398=AXIS2_PLACEMENT_3D('',#58914,#22557,#22558);
#19399=AXIS2_PLACEMENT_3D('',#58916,#22560,#22561);
#19400=AXIS2_PLACEMENT_3D('',#58917,#22562,#22563);
#19401=AXIS2_PLACEMENT_3D('',#58918,#22564,#22565);
#19402=AXIS2_PLACEMENT_3D('',#58919,#22566,#22567);
#19403=AXIS2_PLACEMENT_3D('',#58920,#22568,#22569);
#19404=AXIS2_PLACEMENT_3D('',#58921,#22570,#22571);
#19405=AXIS2_PLACEMENT_3D('',#58922,#22572,#22573);
#19406=AXIS2_PLACEMENT_3D('',#58923,#22574,#22575);
#19407=AXIS2_PLACEMENT_3D('',#58924,#22576,#22577);
#19408=AXIS2_PLACEMENT_3D('',#58926,#22578,#22579);
#19409=AXIS2_PLACEMENT_3D('',#58927,#22580,#22581);
#19410=AXIS2_PLACEMENT_3D('',#58928,#22582,#22583);
#19411=AXIS2_PLACEMENT_3D('',#58929,#22584,#22585);
#19412=AXIS2_PLACEMENT_3D('',#58930,#22586,#22587);
#19413=AXIS2_PLACEMENT_3D('',#58931,#22588,#22589);
#19414=AXIS2_PLACEMENT_3D('',#58932,#22590,#22591);
#19415=AXIS2_PLACEMENT_3D('',#58933,#22592,#22593);
#19416=AXIS2_PLACEMENT_3D('',#58934,#22594,#22595);
#19417=AXIS2_PLACEMENT_3D('',#58935,#22596,#22597);
#19418=AXIS2_PLACEMENT_3D('',#58937,#22598,#22599);
#19419=AXIS2_PLACEMENT_3D('',#58939,#22601,#22602);
#19420=AXIS2_PLACEMENT_3D('',#58941,#22603,#22604);
#19421=AXIS2_PLACEMENT_3D('',#58944,#22606,#22607);
#19422=AXIS2_PLACEMENT_3D('',#58945,#22608,#22609);
#19423=AXIS2_PLACEMENT_3D('',#58947,#22611,#22612);
#19424=AXIS2_PLACEMENT_3D('',#58949,#22614,#22615);
#19425=AXIS2_PLACEMENT_3D('',#58951,#22617,#22618);
#19426=AXIS2_PLACEMENT_3D('',#58953,#22620,#22621);
#19427=AXIS2_PLACEMENT_3D('',#58955,#22623,#22624);
#19428=AXIS2_PLACEMENT_3D('',#58957,#22626,#22627);
#19429=AXIS2_PLACEMENT_3D('',#58959,#22629,#22630);
#19430=AXIS2_PLACEMENT_3D('',#58961,#22632,#22633);
#19431=AXIS2_PLACEMENT_3D('',#58963,#22635,#22636);
#19432=AXIS2_PLACEMENT_3D('',#58965,#22637,#22638);
#19433=AXIS2_PLACEMENT_3D('',#58966,#22639,#22640);
#19434=AXIS2_PLACEMENT_3D('',#58968,#22641,#22642);
#19435=AXIS2_PLACEMENT_3D('',#58970,#22644,#22645);
#19436=AXIS2_PLACEMENT_3D('',#58972,#22646,#22647);
#19437=AXIS2_PLACEMENT_3D('',#58974,#22649,#22650);
#19438=AXIS2_PLACEMENT_3D('',#58976,#22651,#22652);
#19439=AXIS2_PLACEMENT_3D('',#58978,#22654,#22655);
#22434=DIRECTION('axis',(0.,0.,1.));
#22435=DIRECTION('refdir',(1.,0.,0.));
#22436=DIRECTION('center_axis',(0.,0.866025403784439,0.499999999999999));
#22437=DIRECTION('ref_axis',(0.,-0.499999999999999,0.866025403784439));
#22438=DIRECTION('',(-1.,0.,0.));
#22439=DIRECTION('',(0.,0.499999999999999,-0.866025403784439));
#22440=DIRECTION('',(1.,0.,0.));
#22441=DIRECTION('center_axis',(0.,0.996808887069657,-0.0798250753770538));
#22442=DIRECTION('ref_axis',(0.,0.0798250753770538,0.996808887069657));
#22443=DIRECTION('',(1.,0.,0.));
#22444=DIRECTION('',(0.,-0.0798250753770538,-0.996808887069657));
#22445=DIRECTION('center_axis',(0.,0.5,0.866025403784438));
#22446=DIRECTION('ref_axis',(1.,0.,0.));
#22447=DIRECTION('',(-1.,0.,0.));
#22448=DIRECTION('',(0.,0.866025403784438,-0.5));
#22449=DIRECTION('',(1.,0.,0.));
#22450=DIRECTION('center_axis',(0.,0.903174356608943,0.429273900399292));
#22451=DIRECTION('ref_axis',(0.,-0.429273900399292,0.903174356608943));
#22452=DIRECTION('',(1.,0.,0.));
#22453=DIRECTION('',(0.,0.429273900399292,-0.903174356608943));
#22454=DIRECTION('center_axis',(0.,0.,1.));
#22455=DIRECTION('ref_axis',(1.,0.,0.));
#22456=DIRECTION('',(-1.,0.,0.));
#22457=DIRECTION('',(0.,1.,0.));
#22458=DIRECTION('',(1.,0.,0.));
#22459=DIRECTION('center_axis',(0.,0.567534986670364,0.82334928123189));
#22460=DIRECTION('ref_axis',(0.,-0.82334928123189,0.567534986670364));
#22461=DIRECTION('',(1.,0.,0.));
#22462=DIRECTION('',(0.,0.82334928123189,-0.567534986670364));
#22463=DIRECTION('center_axis',(0.,-0.499999999999999,0.866025403784439));
#22464=DIRECTION('ref_axis',(1.,0.,0.));
#22465=DIRECTION('',(-1.,0.,0.));
#22466=DIRECTION('',(0.,0.866025403784439,0.499999999999999));
#22467=DIRECTION('',(1.,0.,0.));
#22468=DIRECTION('center_axis',(0.,0.0798250753770539,0.996808887069657));
#22469=DIRECTION('ref_axis',(0.,-0.996808887069657,0.0798250753770539));
#22470=DIRECTION('',(1.,0.,0.));
#22471=DIRECTION('',(0.,0.996808887069657,-0.0798250753770539));
#22472=DIRECTION('center_axis',(-1.,0.,0.));
#22473=DIRECTION('ref_axis',(0.,-0.707106781186596,0.707106781186499));
#22474=DIRECTION('center_axis',(1.,0.,0.));
#22475=DIRECTION('ref_axis',(0.,1.,0.));
#22476=DIRECTION('center_axis',(0.,-0.866025403784439,0.5));
#22477=DIRECTION('ref_axis',(0.,-0.5,-0.866025403784439));
#22478=DIRECTION('',(-1.,0.,0.));
#22479=DIRECTION('',(0.,0.5,0.866025403784439));
#22480=DIRECTION('',(1.,0.,0.));
#22481=DIRECTION('center_axis',(0.,-0.429273900399292,0.903174356608943));
#22482=DIRECTION('ref_axis',(0.,-0.903174356608943,-0.429273900399292));
#22483=DIRECTION('',(1.,0.,0.));
#22484=DIRECTION('',(0.,0.903174356608943,0.429273900399292));
#22485=DIRECTION('center_axis',(0.,0.500000000000001,-0.866025403784438));
#22486=DIRECTION('ref_axis',(-1.,0.,0.));
#22487=DIRECTION('',(-1.,0.,0.));
#22488=DIRECTION('',(0.,-0.866025403784438,-0.500000000000001));
#22489=DIRECTION('',(1.,0.,0.));
#22490=DIRECTION('center_axis',(0.,-0.0798250753770533,-0.996808887069657));
#22491=DIRECTION('ref_axis',(0.,0.996808887069657,-0.0798250753770533));
#22492=DIRECTION('',(1.,0.,0.));
#22493=DIRECTION('',(0.,-0.996808887069657,0.0798250753770533));
#22494=DIRECTION('center_axis',(0.,0.866025403784438,-0.500000000000001));
#22495=DIRECTION('ref_axis',(-1.,0.,0.));
#22496=DIRECTION('',(-1.,0.,0.));
#22497=DIRECTION('',(0.,-0.500000000000001,-0.866025403784438));
#22498=DIRECTION('',(1.,0.,0.));
#22499=DIRECTION('center_axis',(0.,0.429273900399291,-0.903174356608944));
#22500=DIRECTION('ref_axis',(0.,0.903174356608944,0.429273900399291));
#22501=DIRECTION('',(1.,0.,0.));
#22502=DIRECTION('',(0.,-0.903174356608944,-0.429273900399291));
#22503=DIRECTION('center_axis',(0.,1.,0.));
#22504=DIRECTION('ref_axis',(0.,0.,1.));
#22505=DIRECTION('',(-1.,0.,0.));
#22506=DIRECTION('',(0.,0.,-1.));
#22507=DIRECTION('',(1.,0.,0.));
#22508=DIRECTION('center_axis',(0.,0.82334928123189,-0.567534986670364));
#22509=DIRECTION('ref_axis',(0.,0.567534986670364,0.82334928123189));
#22510=DIRECTION('',(1.,0.,0.));
#22511=DIRECTION('',(0.,-0.567534986670364,-0.82334928123189));
#22512=DIRECTION('center_axis',(0.,-1.,0.));
#22513=DIRECTION('ref_axis',(0.,0.,-1.));
#22514=DIRECTION('',(-1.,0.,0.));
#22515=DIRECTION('',(0.,0.,1.));
#22516=DIRECTION('',(1.,0.,0.));
#22517=DIRECTION('center_axis',(0.,-0.82334928123189,0.567534986670365));
#22518=DIRECTION('ref_axis',(0.,-0.567534986670365,-0.82334928123189));
#22519=DIRECTION('',(1.,0.,0.));
#22520=DIRECTION('',(0.,0.567534986670365,0.82334928123189));
#22521=DIRECTION('center_axis',(0.,-0.866025403784438,-0.5));
#22522=DIRECTION('ref_axis',(-1.,0.,0.));
#22523=DIRECTION('',(-1.,0.,0.));
#22524=DIRECTION('',(0.,-0.5,0.866025403784438));
#22525=DIRECTION('',(1.,0.,0.));
#22526=DIRECTION('center_axis',(0.,-0.996808887069657,0.0798250753770534));
#22527=DIRECTION('ref_axis',(0.,-0.0798250753770534,-0.996808887069657));
#22528=DIRECTION('',(1.,0.,0.));
#22529=DIRECTION('',(0.,0.0798250753770534,0.996808887069657));
#22530=DIRECTION('center_axis',(0.,-0.500000000000001,-0.866025403784438));
#22531=DIRECTION('ref_axis',(-1.,0.,0.));
#22532=DIRECTION('',(-1.,0.,0.));
#22533=DIRECTION('',(0.,-0.866025403784438,0.500000000000001));
#22534=DIRECTION('',(1.,0.,0.));
#22535=DIRECTION('center_axis',(0.,-0.903174356608944,-0.429273900399291));
#22536=DIRECTION('ref_axis',(0.,0.429273900399291,-0.903174356608944));
#22537=DIRECTION('',(1.,0.,0.));
#22538=DIRECTION('',(0.,-0.429273900399291,0.903174356608944));
#22539=DIRECTION('center_axis',(0.,2.24737149820557E-15,-1.));
#22540=DIRECTION('ref_axis',(-1.,0.,0.));
#22541=DIRECTION('',(-1.,0.,0.));
#22542=DIRECTION('',(0.,-1.,-2.24737149820557E-15));
#22543=DIRECTION('',(1.,0.,0.));
#22544=DIRECTION('center_axis',(0.,-0.567534986670365,-0.823349281231889));
#22545=DIRECTION('ref_axis',(0.,0.823349281231889,-0.567534986670365));
#22546=DIRECTION('',(1.,0.,0.));
#22547=DIRECTION('',(0.,-0.823349281231889,0.567534986670365));
#22548=DIRECTION('center_axis',(0.,0.567534986670365,-0.82334928123189));
#22549=DIRECTION('ref_axis',(0.,0.823349281231889,0.567534986670365));
#22550=DIRECTION('',(0.,-0.823349281231889,-0.567534986670365));
#22551=DIRECTION('center_axis',(0.,0.0798250753770525,-0.996808887069657));
#22552=DIRECTION('ref_axis',(0.,0.996808887069657,0.0798250753770525));
#22553=DIRECTION('',(0.,-0.996808887069657,-0.0798250753770525));
#22554=DIRECTION('center_axis',(0.,-0.429273900399292,-0.903174356608943));
#22555=DIRECTION('ref_axis',(0.,0.903174356608943,-0.429273900399292));
#22556=DIRECTION('',(0.,-0.903174356608943,0.429273900399292));
#22557=DIRECTION('center_axis',(0.,-0.82334928123189,-0.567534986670364));
#22558=DIRECTION('ref_axis',(0.,0.567534986670364,-0.82334928123189));
#22559=DIRECTION('',(0.,-0.567534986670364,0.82334928123189));
#22560=DIRECTION('center_axis',(1.,0.,0.));
#22561=DIRECTION('ref_axis',(0.,0.,-1.));
#22562=DIRECTION('center_axis',(1.,0.,0.));
#22563=DIRECTION('ref_axis',(0.,1.,0.));
#22564=DIRECTION('center_axis',(1.,0.,0.));
#22565=DIRECTION('ref_axis',(0.,1.,0.));
#22566=DIRECTION('center_axis',(1.,0.,0.));
#22567=DIRECTION('ref_axis',(0.,1.,0.));
#22568=DIRECTION('center_axis',(1.,0.,0.));
#22569=DIRECTION('ref_axis',(0.,1.,0.));
#22570=DIRECTION('center_axis',(1.,0.,0.));
#22571=DIRECTION('ref_axis',(0.,1.,0.));
#22572=DIRECTION('center_axis',(1.,0.,0.));
#22573=DIRECTION('ref_axis',(0.,1.,0.));
#22574=DIRECTION('center_axis',(1.,0.,0.));
#22575=DIRECTION('ref_axis',(0.,1.,0.));
#22576=DIRECTION('center_axis',(1.,0.,0.));
#22577=DIRECTION('ref_axis',(0.,1.,0.));
#22578=DIRECTION('center_axis',(-1.,0.,0.));
#22579=DIRECTION('ref_axis',(0.,1.,0.));
#22580=DIRECTION('center_axis',(-1.,0.,0.));
#22581=DIRECTION('ref_axis',(0.,1.,0.));
#22582=DIRECTION('center_axis',(-1.,0.,0.));
#22583=DIRECTION('ref_axis',(0.,1.,0.));
#22584=DIRECTION('center_axis',(-1.,0.,0.));
#22585=DIRECTION('ref_axis',(0.,1.,0.));
#22586=DIRECTION('center_axis',(-1.,0.,0.));
#22587=DIRECTION('ref_axis',(0.,1.,0.));
#22588=DIRECTION('center_axis',(-1.,0.,0.));
#22589=DIRECTION('ref_axis',(0.,1.,0.));
#22590=DIRECTION('center_axis',(-1.,0.,0.));
#22591=DIRECTION('ref_axis',(0.,1.,0.));
#22592=DIRECTION('center_axis',(-1.,0.,0.));
#22593=DIRECTION('ref_axis',(0.,1.,0.));
#22594=DIRECTION('center_axis',(-1.,0.,0.));
#22595=DIRECTION('ref_axis',(0.,1.,0.));
#22596=DIRECTION('center_axis',(1.,0.,0.));
#22597=DIRECTION('ref_axis',(0.,1.,0.));
#22598=DIRECTION('center_axis',(1.,0.,0.));
#22599=DIRECTION('ref_axis',(0.,1.,0.));
#22600=DIRECTION('',(0.707106781186548,-0.707106781186547,-8.65956056235493E-17));
#22601=DIRECTION('center_axis',(-1.,0.,0.));
#22602=DIRECTION('ref_axis',(0.,1.,0.));
#22603=DIRECTION('center_axis',(1.,0.,0.));
#22604=DIRECTION('ref_axis',(0.,1.,0.));
#22605=DIRECTION('',(0.707106781186547,0.707106781186547,8.65956056235493E-17));
#22606=DIRECTION('center_axis',(-1.,0.,0.));
#22607=DIRECTION('ref_axis',(0.,1.,0.));
#22608=DIRECTION('center_axis',(0.,0.996808887069657,0.0798250753770525));
#22609=DIRECTION('ref_axis',(0.,-0.0798250753770525,0.996808887069657));
#22610=DIRECTION('',(0.,0.0798250753770525,-0.996808887069657));
#22611=DIRECTION('center_axis',(0.,0.903174356608943,-0.429273900399292));
#22612=DIRECTION('ref_axis',(0.,0.429273900399292,0.903174356608943));
#22613=DIRECTION('',(0.,-0.429273900399292,-0.903174356608943));
#22614=DIRECTION('center_axis',(0.,-0.996808887069657,-0.0798250753770546));
#22615=DIRECTION('ref_axis',(0.,0.0798250753770546,-0.996808887069657));
#22616=DIRECTION('',(0.,-0.0798250753770546,0.996808887069657));
#22617=DIRECTION('center_axis',(0.,-0.903174356608943,0.429273900399292));
#22618=DIRECTION('ref_axis',(0.,-0.429273900399292,-0.903174356608943));
#22619=DIRECTION('',(0.,0.429273900399292,0.903174356608943));
#22620=DIRECTION('center_axis',(0.,-0.567534986670364,0.82334928123189));
#22621=DIRECTION('ref_axis',(0.,-0.82334928123189,-0.567534986670364));
#22622=DIRECTION('',(0.,0.82334928123189,0.567534986670364));
#22623=DIRECTION('center_axis',(0.,-0.0798250753770534,0.996808887069657));
#22624=DIRECTION('ref_axis',(0.,-0.996808887069657,-0.0798250753770534));
#22625=DIRECTION('',(0.,0.996808887069657,0.0798250753770534));
#22626=DIRECTION('center_axis',(0.,0.429273900399292,0.903174356608943));
#22627=DIRECTION('ref_axis',(0.,-0.903174356608943,0.429273900399292));
#22628=DIRECTION('',(0.,0.903174356608943,-0.429273900399292));
#22629=DIRECTION('center_axis',(0.,0.82334928123189,0.567534986670364));
#22630=DIRECTION('ref_axis',(0.,-0.567534986670364,0.82334928123189));
#22631=DIRECTION('',(0.,0.567534986670364,-0.82334928123189));
#22632=DIRECTION('center_axis',(1.,0.,0.));
#22633=DIRECTION('ref_axis',(0.,1.,0.));
#22634=DIRECTION('',(-1.,0.,0.));
#22635=DIRECTION('center_axis',(-1.,0.,0.));
#22636=DIRECTION('ref_axis',(0.,0.,1.));
#22637=DIRECTION('center_axis',(1.,0.,0.));
#22638=DIRECTION('ref_axis',(0.,0.,-1.));
#22639=DIRECTION('center_axis',(1.,0.,0.));
#22640=DIRECTION('ref_axis',(0.,1.,0.));
#22641=DIRECTION('center_axis',(1.,0.,0.));
#22642=DIRECTION('ref_axis',(0.,0.,-1.));
#22643=DIRECTION('',(-0.707106781186547,0.707106781186548,8.65956056235494E-17));
#22644=DIRECTION('center_axis',(1.,0.,0.));
#22645=DIRECTION('ref_axis',(0.,1.,0.));
#22646=DIRECTION('center_axis',(1.,0.,0.));
#22647=DIRECTION('ref_axis',(0.,0.,-1.));
#22648=DIRECTION('',(-1.,0.,0.));
#22649=DIRECTION('center_axis',(-1.,0.,0.));
#22650=DIRECTION('ref_axis',(0.,1.,0.));
#22651=DIRECTION('center_axis',(1.,0.,0.));
#22652=DIRECTION('ref_axis',(0.,0.,-1.));
#22653=DIRECTION('',(-0.371390676354104,-0.928476690885259,-1.13705600757556E-16));
#22654=DIRECTION('center_axis',(1.,0.,0.));
#22655=DIRECTION('ref_axis',(0.,0.,-1.));
#57382=CARTESIAN_POINT('',(0.,0.,0.));
#57383=CARTESIAN_POINT('Origin',(1.5,4.65899107620574,2.68986975199944));
#57384=CARTESIAN_POINT('',(6.68133955674308,4.65899107620048,2.68986975199644));
#57385=CARTESIAN_POINT('',(6.4964847157299,4.78249346839053,2.47595733387918));
#57386=CARTESIAN_POINT('Ctrl Pts',(6.68133955674087,4.65899107619594,2.6898697519957));
#57387=CARTESIAN_POINT('Ctrl Pts',(6.67492308098284,4.66333926734057,2.68233846075464));
#57388=CARTESIAN_POINT('Ctrl Pts',(6.6685005684247,4.6676851311398,2.67481117074313));
#57389=CARTESIAN_POINT('Ctrl Pts',(6.6620720344556,4.67202864152121,2.66728791952006));
#57390=CARTESIAN_POINT('Ctrl Pts',(6.6073292890925,4.70901618548297,2.60322301327753));
#57391=CARTESIAN_POINT('Ctrl Pts',(6.55213434648286,4.74584349646411,2.53943317427317));
#57392=CARTESIAN_POINT('Ctrl Pts',(6.49649612060902,4.78249290359719,2.47595028107013));
#57393=CARTESIAN_POINT('',(1.6,4.78249346839052,2.4759573338791));
#57394=CARTESIAN_POINT('',(1.5,4.78249346839052,2.4759573338791));
#57395=CARTESIAN_POINT('',(1.6,4.53548868402095,2.90378217011979));
#57396=CARTESIAN_POINT('',(1.6,5.10274107620574,1.92127220614075));
#57397=CARTESIAN_POINT('',(6.49648471573067,4.53548868402103,2.90378217011975));
#57398=CARTESIAN_POINT('',(1.5,4.53548868402095,2.90378217011979));
#57399=CARTESIAN_POINT('Ctrl Pts',(6.49648471573075,4.53548868402095,2.90378217011979));
#57400=CARTESIAN_POINT('Ctrl Pts',(6.55337396234634,4.57295850701816,2.83888253293802));
#57401=CARTESIAN_POINT('Ctrl Pts',(6.60979834671122,4.61061413969367,2.77366106395288));
#57402=CARTESIAN_POINT('Ctrl Pts',(6.67094806990306,4.65195340556208,2.70205935512119));
#57403=CARTESIAN_POINT('Ctrl Pts',(6.67614580655144,4.65547147830345,2.69596587438841));
#57404=CARTESIAN_POINT('Ctrl Pts',(6.68133955672778,4.65899107621137,2.68986975198969));
#57405=CARTESIAN_POINT('Origin',(1.5,4.68474025750198,1.25527236874723));
#57406=CARTESIAN_POINT('',(6.9730266888256,4.68474025754297,1.25527236925909));
#57407=CARTESIAN_POINT('Ctrl Pts',(6.97303770557678,4.68473984672734,1.25526723923358));
#57408=CARTESIAN_POINT('Ctrl Pts',(6.85768162673857,4.71538888116549,1.63799446828719));
#57409=CARTESIAN_POINT('Ctrl Pts',(6.70189613372097,4.74746137538506,2.03849703114157));
#57410=CARTESIAN_POINT('Ctrl Pts',(6.49649612060898,4.7824929035972,2.47595028107023));
#57411=CARTESIAN_POINT('',(1.6,4.68474025750198,1.25527236874723));
#57412=CARTESIAN_POINT('',(1.5,4.68474025750198,1.25527236874723));
#57413=CARTESIAN_POINT('',(1.6,4.63118372339748,0.586489672284435));
#57414=CARTESIAN_POINT('Ctrl Pts',(6.45213506683142,4.78997609487978,2.5693960002115));
#57415=CARTESIAN_POINT('Ctrl Pts',(6.69496761877087,4.74945078078581,2.06333956306629));
#57416=CARTESIAN_POINT('Ctrl Pts',(6.87214261929782,4.7129326345547,1.60732229617945));
#57417=CARTESIAN_POINT('Ctrl Pts',(6.99737260418699,4.67812918220736,1.17271712435015));
#57418=CARTESIAN_POINT('Ctrl Pts',(6.59045151583296,4.71093147065315,2.6420974655224));
#57419=CARTESIAN_POINT('Ctrl Pts',(6.83894619948317,4.67186091612313,2.13090865278462));
#57420=CARTESIAN_POINT('Ctrl Pts',(7.02199092230211,4.63669438947174,1.6676886040292));
#57421=CARTESIAN_POINT('Ctrl Pts',(7.15213252925719,4.60270344939976,1.22335080384112));
#57422=CARTESIAN_POINT('Ctrl Pts',(6.7287679648345,4.63188684642653,2.7147989308333));
#57423=CARTESIAN_POINT('Ctrl Pts',(6.98292478019547,4.59427105146045,2.19847774250294));
#57424=CARTESIAN_POINT('Ctrl Pts',(7.17183922530641,4.56045614438878,1.72805491187896));
#57425=CARTESIAN_POINT('Ctrl Pts',(7.30689245432738,4.52727771659216,1.27398448333209));
#57426=CARTESIAN_POINT('Ctrl Pts',(6.86708441383604,4.5528422221999,2.7875003961442));
#57427=CARTESIAN_POINT('Ctrl Pts',(7.12690336090777,4.51668118679778,2.26604683222127));
#57428=CARTESIAN_POINT('Ctrl Pts',(7.32168752831071,4.48421789930582,1.78842121972871));
#57429=CARTESIAN_POINT('Ctrl Pts',(7.46165237939758,4.45185198378456,1.32461816282306));
#57430=CARTESIAN_POINT('',(6.94805436450009,4.54138228956796,2.62196828737462));
#57431=CARTESIAN_POINT('Ctrl Pts',(6.94805436450009,4.54138228956796,2.62196828737462));
#57432=CARTESIAN_POINT('Ctrl Pts',(6.85888718065088,4.58048619487533,2.64454493763046));
#57433=CARTESIAN_POINT('Ctrl Pts',(6.7680729844652,4.62053162275365,2.66766517619599));
#57434=CARTESIAN_POINT('Ctrl Pts',(6.68133955674308,4.65899107619524,2.68986975199342));
#57435=CARTESIAN_POINT('',(7.46165237939758,4.45185198378456,1.32461816282306));
#57436=CARTESIAN_POINT('Ctrl Pts',(6.94809164225473,4.54138208596012,2.62194359089516));
#57437=CARTESIAN_POINT('Ctrl Pts',(7.16787076968256,4.50975040784356,2.16421694982278));
#57438=CARTESIAN_POINT('Ctrl Pts',(7.33663088231394,4.4807623507912,1.73890326423272));
#57439=CARTESIAN_POINT('Ctrl Pts',(7.46165237939758,4.45185198378456,1.32461816282306));
#57440=CARTESIAN_POINT('',(7.17384635845297,4.59212072600797,1.23045504008007));
#57441=CARTESIAN_POINT('Ctrl Pts',(7.46165237939758,4.45185198378456,1.32461816282306));
#57442=CARTESIAN_POINT('Ctrl Pts',(7.36571703908271,4.49860823119237,1.29323045524206));
#57443=CARTESIAN_POINT('Ctrl Pts',(7.26978169876784,4.54536447860017,1.26184274766107));
#57444=CARTESIAN_POINT('Ctrl Pts',(7.17384635845297,4.59212072600797,1.23045504008007));
#57445=CARTESIAN_POINT('Ctrl Pts',(7.17384635845264,4.59212072600813,1.23045504008011));
#57446=CARTESIAN_POINT('Ctrl Pts',(7.10373004606762,4.62436150671956,1.23909393123514));
#57447=CARTESIAN_POINT('Ctrl Pts',(7.04027818843215,4.65362469478555,1.24693497884549));
#57448=CARTESIAN_POINT('Ctrl Pts',(6.97302668796278,4.68474025804403,1.25527236889283));
#57449=CARTESIAN_POINT('Origin',(1.5,2.68986975199945,4.65899107620574));
#57450=CARTESIAN_POINT('',(6.68133955674308,2.6898697519964,4.65899107620051));
#57451=CARTESIAN_POINT('',(6.4964847157299,2.90378217011975,4.53548868402103));
#57452=CARTESIAN_POINT('Ctrl Pts',(6.68133955674087,2.68986975199284,4.65899107619759));
#57453=CARTESIAN_POINT('Ctrl Pts',(6.67492308098284,2.69740104160513,4.65464288223185));
#57454=CARTESIAN_POINT('Ctrl Pts',(6.6685005684247,2.7049283150624,4.65029698975985));
#57455=CARTESIAN_POINT('Ctrl Pts',(6.6620720344556,2.71245153100584,4.64595341827232));
#57456=CARTESIAN_POINT('Ctrl Pts',(6.60732928909252,2.77651613682155,4.60896535395611));
#57457=CARTESIAN_POINT('Ctrl Pts',(6.55213434648287,2.84030444318649,4.57213538836559));
#57458=CARTESIAN_POINT('Ctrl Pts',(6.49649612060902,2.9037852073989,4.53548229371255));
#57459=CARTESIAN_POINT('',(1.6,2.90378217011979,4.53548868402095));
#57460=CARTESIAN_POINT('',(1.5,2.90378217011979,4.53548868402095));
#57461=CARTESIAN_POINT('',(1.6,2.4759573338791,4.78249346839052));
#57462=CARTESIAN_POINT('',(1.6,4.02111975199945,3.89039353034704));
#57463=CARTESIAN_POINT('',(6.49648471573067,2.47595733387918,4.78249346839053));
#57464=CARTESIAN_POINT('',(1.5,2.4759573338791,4.78249346839052));
#57465=CARTESIAN_POINT('Ctrl Pts',(6.49648471573075,2.4759573338791,4.78249346839052));
#57466=CARTESIAN_POINT('Ctrl Pts',(6.55337396234642,2.54085697106096,4.74502364539326));
#57467=CARTESIAN_POINT('Ctrl Pts',(6.60979834671138,2.6060784400462,4.7073680127177));
#57468=CARTESIAN_POINT('Ctrl Pts',(6.67094806990306,2.67768014887771,4.66602874684939));
#57469=CARTESIAN_POINT('Ctrl Pts',(6.67614580655144,2.68377362961048,4.66251067410802));
#57470=CARTESIAN_POINT('Ctrl Pts',(6.68133955672777,2.6898697520092,4.6589910762001));
#57471=CARTESIAN_POINT('Origin',(1.5,3.42946788875476,3.42946788875476));
#57472=CARTESIAN_POINT('',(6.9730266888256,3.42946788853432,3.42946788921854));
#57473=CARTESIAN_POINT('Ctrl Pts',(6.97303770557678,3.4294700977703,3.42946324107831));
#57474=CARTESIAN_POINT('Ctrl Pts',(6.85768162673857,3.26464932566841,3.77623926137783));
#57475=CARTESIAN_POINT('Ctrl Pts',(6.70189613372098,3.09217363899809,4.13912090220029));
#57476=CARTESIAN_POINT('Ctrl Pts',(6.49649612060898,2.90378520739886,4.53548229371264));
#57477=CARTESIAN_POINT('',(1.6,3.42946788875476,3.42946788875476));
#57478=CARTESIAN_POINT('',(1.5,3.42946788875476,3.42946788875476));
#57479=CARTESIAN_POINT('',(1.6,4.10539157077492,2.00735269363697));
#57480=CARTESIAN_POINT('Ctrl Pts',(6.45213506683141,2.86354298158031,4.62015025600519));
#57481=CARTESIAN_POINT('Ctrl Pts',(6.69496761877087,3.08147524865119,4.16162986864181));
#57482=CARTESIAN_POINT('Ctrl Pts',(6.87214261929781,3.27785823975936,3.74844825783789));
#57483=CARTESIAN_POINT('Ctrl Pts',(6.99737260418699,3.46502015180182,3.35466741224394));
#57484=CARTESIAN_POINT('Ctrl Pts',(6.59045151583295,2.758737596312,4.64358925974348));
#57485=CARTESIAN_POINT('Ctrl Pts',(6.83894619948317,2.98049590991795,4.18135148451713));
#57486=CARTESIAN_POINT('Ctrl Pts',(7.02199092230211,3.1816508288527,3.76260789142697));
#57487=CARTESIAN_POINT('Ctrl Pts',(7.15213252925719,3.37438271134589,3.3608045985664));
#57488=CARTESIAN_POINT('Ctrl Pts',(6.72876796483449,2.6539322110437,4.66702826348176));
#57489=CARTESIAN_POINT('Ctrl Pts',(6.98292478019547,2.87951657118472,4.20107310039245));
#57490=CARTESIAN_POINT('Ctrl Pts',(7.17183922530641,3.08544341794604,3.77676752501605));
#57491=CARTESIAN_POINT('Ctrl Pts',(7.30689245432738,3.28374527088997,3.36694178488886));
#57492=CARTESIAN_POINT('Ctrl Pts',(6.86708441383603,2.54912682577539,4.69046726722004));
#57493=CARTESIAN_POINT('Ctrl Pts',(7.12690336090777,2.77853723245148,4.22079471626778));
#57494=CARTESIAN_POINT('Ctrl Pts',(7.3216875283107,2.98923600703937,3.79092715860513));
#57495=CARTESIAN_POINT('Ctrl Pts',(7.46165237939758,3.19310783043405,3.37307897121132));
#57496=CARTESIAN_POINT('',(6.94805436450009,2.62196828737528,4.54138228956758));
#57497=CARTESIAN_POINT('Ctrl Pts',(6.94805436450009,2.62196828737528,4.54138228956758));
#57498=CARTESIAN_POINT('Ctrl Pts',(6.85888711552653,2.64454495411986,4.58048622343519));
#57499=CARTESIAN_POINT('Ctrl Pts',(6.76807293638612,2.6676651885047,4.62053164407293));
#57500=CARTESIAN_POINT('Ctrl Pts',(6.68133955674307,2.68986975199337,4.65899107619527));
#57501=CARTESIAN_POINT('',(7.46165237939758,3.19310783043405,3.37307897121132));
#57502=CARTESIAN_POINT('Ctrl Pts',(6.94809164225473,2.62198045928545,4.54136079998506));
#57503=CARTESIAN_POINT('Ctrl Pts',(7.16787076968256,2.82344994300837,4.12914206176917));
#57504=CARTESIAN_POINT('Ctrl Pts',(7.33663088231394,3.0110023919897,3.74631557694482));
#57505=CARTESIAN_POINT('Ctrl Pts',(7.46165237939758,3.19310783043405,3.37307897121132));
#57506=CARTESIAN_POINT('',(7.17384635845298,3.3616656859279,3.36166568592793));
#57507=CARTESIAN_POINT('Ctrl Pts',(7.46165237939758,3.19310783043405,3.37307897121132));
#57508=CARTESIAN_POINT('Ctrl Pts',(7.36571703908271,3.24929378226533,3.36927454278352));
#57509=CARTESIAN_POINT('Ctrl Pts',(7.26978169876785,3.30547973409662,3.36547011435573));
#57510=CARTESIAN_POINT('Ctrl Pts',(7.17384635845298,3.3616656859279,3.36166568592793));
#57511=CARTESIAN_POINT('Ctrl Pts',(7.17384635845271,3.361665685928,3.36166568592802));
#57512=CARTESIAN_POINT('Ctrl Pts',(7.10380439458403,3.38524254899043,3.38524254899052));
#57513=CARTESIAN_POINT('Ctrl Pts',(7.04024193630147,3.40670199458556,3.4067019945858));
#57514=CARTESIAN_POINT('Ctrl Pts',(6.9730266882762,3.42946788904522,3.42946788904572));
#57515=CARTESIAN_POINT('Origin',(1.5,2.60208521396521E-16,5.37973950399889));
#57516=CARTESIAN_POINT('',(6.68133955674308,-2.66020618484513E-14,5.37973950399284));
#57517=CARTESIAN_POINT('',(6.4964847157299,0.2470047843695,5.37973950399894));
#57518=CARTESIAN_POINT('Ctrl Pts',(6.68133955674087,-1.6530180002583E-12,
5.37973950398853));
#57519=CARTESIAN_POINT('Ctrl Pts',(6.67492308098284,0.00869638510872298,
5.37973950235977));
#57520=CARTESIAN_POINT('Ctrl Pts',(6.6685005684247,0.0173881413799499,5.37973948580553));
#57521=CARTESIAN_POINT('Ctrl Pts',(6.6620720344556,0.0260752232488897,5.3797394505259));
#57522=CARTESIAN_POINT('Ctrl Pts',(6.60732928909258,0.100050831526762,5.37973915009911));
#57523=CARTESIAN_POINT('Ctrl Pts',(6.5521343464829,0.173708108098482,5.37973761745967));
#57524=CARTESIAN_POINT('Ctrl Pts',(6.49649612060902,0.247010609884639,5.37973548846904));
#57525=CARTESIAN_POINT('',(1.6,0.247004784369567,5.37973950399889));
#57526=CARTESIAN_POINT('',(1.5,0.247004784369567,5.37973950399889));
#57527=CARTESIAN_POINT('',(1.6,-0.247004784369566,5.37973950399889));
#57528=CARTESIAN_POINT('',(1.6,1.775,5.37973950399889));
#57529=CARTESIAN_POINT('',(6.49648471573025,-0.247004784369127,5.37973950399919));
#57530=CARTESIAN_POINT('',(1.5,-0.247004784369566,5.37973950399889));
#57531=CARTESIAN_POINT('Ctrl Pts',(6.49648471573075,-0.247004784369566,
5.37973950399889));
#57532=CARTESIAN_POINT('Ctrl Pts',(6.5534522954077,-0.171961951002559,5.37973950399889));
#57533=CARTESIAN_POINT('Ctrl Pts',(6.60995374323598,-0.0965464591095595,
5.37973950399889));
#57534=CARTESIAN_POINT('Ctrl Pts',(6.67110204921906,-0.013866898540887,
5.37973950399889));
#57535=CARTESIAN_POINT('Ctrl Pts',(6.67622273755884,-0.00693492963715604,
5.37973950399889));
#57536=CARTESIAN_POINT('Ctrl Pts',(6.68133955672777,1.12630738069441E-11,
5.37973950399889));
#57537=CARTESIAN_POINT('Origin',(1.5,1.25527236874723,4.68474025750198));
#57538=CARTESIAN_POINT('',(6.9730266888256,1.25527236832443,4.68474025779341));
#57539=CARTESIAN_POINT('Ctrl Pts',(6.97303770557678,1.25527660564903,4.68473733700388));
#57540=CARTESIAN_POINT('Ctrl Pts',(6.85768162673857,0.93914961978766,4.90264379395559));
#57541=CARTESIAN_POINT('Ctrl Pts',(6.70189613372097,0.608340473184774,5.13067067013966));
#57542=CARTESIAN_POINT('Ctrl Pts',(6.49649612060898,0.247010609884559,5.37973548846909));
#57543=CARTESIAN_POINT('',(1.6,1.25527236874723,4.68474025750198));
#57544=CARTESIAN_POINT('',(1.5,1.25527236874723,4.68474025750198));
#57545=CARTESIAN_POINT('',(1.6,3.12761653072357,3.39413268276809));
#57546=CARTESIAN_POINT('Ctrl Pts',(6.45213506683129,0.169825838874388,5.43293898179196));
#57547=CARTESIAN_POINT('Ctrl Pts',(6.69496761877081,0.587820912143886,5.14481481171758));
#57548=CARTESIAN_POINT('Ctrl Pts',(6.87214261929779,0.964484376716749,4.88518053593885));
#57549=CARTESIAN_POINT('Ctrl Pts',(6.99737260418699,1.32346176996342,4.63773727615197));
#57550=CARTESIAN_POINT('Ctrl Pts',(6.59045151583283,0.0673422109094778,
5.40083506183456));
#57551=CARTESIAN_POINT('Ctrl Pts',(6.83894619948311,0.490509431605883,5.11140456270267));
#57552=CARTESIAN_POINT('Ctrl Pts',(7.02199092230209,0.874086498044711,4.84933943288195));
#57553=CARTESIAN_POINT('Ctrl Pts',(7.15213252925719,1.24189885083336,4.59773351518701));
#57554=CARTESIAN_POINT('Ctrl Pts',(6.72876796483437,-0.0351414170554326,
5.36873114187716));
#57555=CARTESIAN_POINT('Ctrl Pts',(6.98292478019541,0.39319795106788,5.07799431368776));
#57556=CARTESIAN_POINT('Ctrl Pts',(7.17183922530639,0.783688619372672,4.81349832982504));
#57557=CARTESIAN_POINT('Ctrl Pts',(7.30689245432738,1.1603359317033,4.55772975422206));
#57558=CARTESIAN_POINT('Ctrl Pts',(6.86708441383591,-0.137625045020343,
5.33662722191976));
#57559=CARTESIAN_POINT('Ctrl Pts',(7.12690336090771,0.295886470529877,5.04458406467285));
#57560=CARTESIAN_POINT('Ctrl Pts',(7.32168752831068,0.693290740700634,4.77765722676813));
#57561=CARTESIAN_POINT('Ctrl Pts',(7.46165237939758,1.07877301257324,4.51772599325711));
#57562=CARTESIAN_POINT('',(6.94805436450009,3.7775338412871E-13,5.2439365747499));
#57563=CARTESIAN_POINT('Ctrl Pts',(6.94805436450009,3.78588122203372E-13,
5.2439365747499));
#57564=CARTESIAN_POINT('Ctrl Pts',(6.85888652980283,1.57378817050387E-13,
5.28909020484362));
#57565=CARTESIAN_POINT('Ctrl Pts',(6.76807250396889,2.03924805264334E-15,
5.33533059841517));
#57566=CARTESIAN_POINT('Ctrl Pts',(6.68133955674308,-2.8570895649338E-14,
5.37973950398679));
#57567=CARTESIAN_POINT('',(7.46165237939758,1.07877301257324,4.51772599325711));
#57568=CARTESIAN_POINT('Ctrl Pts',(6.94809164225473,2.12859750591682E-5,
5.24392405018061));
#57569=CARTESIAN_POINT('Ctrl Pts',(7.16787076968256,0.380608346074387,4.98766689283114));
#57570=CARTESIAN_POINT('Ctrl Pts',(7.33663088231394,0.734446773846381,4.74990565622242));
#57571=CARTESIAN_POINT('Ctrl Pts',(7.46165237939758,1.07877301257324,4.51772599325711));
#57572=CARTESIAN_POINT('',(7.17384635845298,1.23045504008004,4.59212072600798));
#57573=CARTESIAN_POINT('Ctrl Pts',(7.46165237939758,1.07877301257324,4.51772599325711));
#57574=CARTESIAN_POINT('Ctrl Pts',(7.36571703908271,1.12933368840884,4.5425242375074));
#57575=CARTESIAN_POINT('Ctrl Pts',(7.26978169876785,1.17989436424444,4.56732248175769));
#57576=CARTESIAN_POINT('Ctrl Pts',(7.17384635845298,1.23045504008004,4.59212072600798));
#57577=CARTESIAN_POINT('Ctrl Pts',(7.17384635845272,1.23045504008007,4.5921207260081));
#57578=CARTESIAN_POINT('Ctrl Pts',(7.10380410095029,1.23908480708047,4.62432745491123));
#57579=CARTESIAN_POINT('Ctrl Pts',(7.04024207626729,1.24693945578929,4.65364140296857));
#57580=CARTESIAN_POINT('Ctrl Pts',(6.9730266882762,1.2552723688533,4.6847402578992));
#57581=CARTESIAN_POINT('Origin',(1.5,-2.68986975199944,4.65899107620574));
#57582=CARTESIAN_POINT('',(6.82679400487526,-2.90378217011979,4.53548868402095));
#57583=CARTESIAN_POINT('',(6.82679400487407,-2.4759573338791,4.78249346839052));
#57584=CARTESIAN_POINT('Ctrl Pts',(6.82679400487526,-2.90378217011979,4.53548868402095));
#57585=CARTESIAN_POINT('Ctrl Pts',(6.83650459025506,-2.68986975199908,4.65899107620594));
#57586=CARTESIAN_POINT('Ctrl Pts',(6.82679400487407,-2.4759573338791,4.78249346839052));
#57587=CARTESIAN_POINT('',(1.6,-2.4759573338791,4.78249346839052));
#57588=CARTESIAN_POINT('',(1.5,-2.4759573338791,4.78249346839052));
#57589=CARTESIAN_POINT('',(1.6,-2.90378217011979,4.53548868402095));
#57590=CARTESIAN_POINT('',(1.6,-1.35861975199944,5.42758862206442));
#57591=CARTESIAN_POINT('',(1.5,-2.90378217011979,4.53548868402095));
#57592=CARTESIAN_POINT('Origin',(1.5,-1.25527236874723,4.68474025750198));
#57593=CARTESIAN_POINT('',(7.28571428571429,-1.25527236874723,4.68474025750198));
#57594=CARTESIAN_POINT('Ctrl Pts',(6.82679400487407,-2.4759573338791,4.78249346839052));
#57595=CARTESIAN_POINT('Ctrl Pts',(7.11904573622593,-1.83368826213753,4.7310601618368));
#57596=CARTESIAN_POINT('Ctrl Pts',(7.28571428571429,-1.25527236874723,4.68474025750198));
#57597=CARTESIAN_POINT('',(7.38335469474708,-0.875998372174533,4.65436776006772));
#57598=CARTESIAN_POINT('Ctrl Pts',(7.28571428571429,-1.25527236874723,4.68474025750198));
#57599=CARTESIAN_POINT('Ctrl Pts',(7.34100687338275,-1.06338186755404,4.6693735468711));
#57600=CARTESIAN_POINT('Ctrl Pts',(7.38335469474708,-0.875998372174533,
4.65436776006772));
#57601=CARTESIAN_POINT('',(6.97302668913468,-1.25527236874723,4.68474025750198));
#57602=CARTESIAN_POINT('Ctrl Pts',(7.38335469474708,-0.875998372174534,
4.65436776006772));
#57603=CARTESIAN_POINT('Ctrl Pts',(7.3156799620785,-0.939686273403086,4.65946792679188));
#57604=CARTESIAN_POINT('Ctrl Pts',(7.24771026860098,-1.00309430560521,4.6645456814304));
#57605=CARTESIAN_POINT('Ctrl Pts',(7.1109529188272,-1.12952063537562,4.67466998051569));
#57606=CARTESIAN_POINT('Ctrl Pts',(7.04212976986549,-1.19256708728131,4.6797187795793));
#57607=CARTESIAN_POINT('Ctrl Pts',(6.97302668913468,-1.25527236874723,4.68474025750198));
#57608=CARTESIAN_POINT('',(1.6,-1.25527236874723,4.68474025750198));
#57609=CARTESIAN_POINT('',(1.5,-1.25527236874723,4.68474025750198));
#57610=CARTESIAN_POINT('',(1.6,1.31843731356659,4.47863598610718));
#57611=CARTESIAN_POINT('Origin',(6.9,0.,0.));
#57612=CARTESIAN_POINT('',(7.28571428571429,-3.42946788875475,3.42946788875476));
#57613=CARTESIAN_POINT('Ctrl Pts',(7.28571428571429,-3.42946788875475,3.42946788875476));
#57614=CARTESIAN_POINT('Ctrl Pts',(7.11904573622629,-3.18037415591191,3.95355069855613));
#57615=CARTESIAN_POINT('Ctrl Pts',(6.82679400487526,-2.90378217011979,4.53548868402095));
#57616=CARTESIAN_POINT('',(6.82679400487407,-4.53548868402095,2.90378217011979));
#57617=CARTESIAN_POINT('Ctrl Pts',(6.82679400487407,-4.53548868402095,2.90378217011979));
#57618=CARTESIAN_POINT('Ctrl Pts',(7.11904573622593,-3.95355069855084,3.18037415591442));
#57619=CARTESIAN_POINT('Ctrl Pts',(7.28571428571429,-3.42946788875475,3.42946788875476));
#57620=CARTESIAN_POINT('',(6.82679400487526,-4.78249346839052,2.4759573338791));
#57621=CARTESIAN_POINT('Ctrl Pts',(6.82679400487526,-4.78249346839052,2.4759573338791));
#57622=CARTESIAN_POINT('Ctrl Pts',(6.83650459025506,-4.65899107620553,2.68986975199981));
#57623=CARTESIAN_POINT('Ctrl Pts',(6.82679400487407,-4.53548868402095,2.90378217011979));
#57624=CARTESIAN_POINT('',(7.28571428571429,-4.68474025750198,1.25527236874723));
#57625=CARTESIAN_POINT('Ctrl Pts',(7.28571428571429,-4.68474025750198,1.25527236874723));
#57626=CARTESIAN_POINT('Ctrl Pts',(7.11904573622629,-4.73106016183727,1.83368826214337));
#57627=CARTESIAN_POINT('Ctrl Pts',(6.82679400487526,-4.78249346839052,2.4759573338791));
#57628=CARTESIAN_POINT('',(7.38335469474695,-4.65436776006777,0.875998372175109));
#57629=CARTESIAN_POINT('Ctrl Pts',(7.38335469474695,-4.65436776006777,0.875998372175109));
#57630=CARTESIAN_POINT('Ctrl Pts',(7.34100687338272,-4.66937354687111,1.06338186755417));
#57631=CARTESIAN_POINT('Ctrl Pts',(7.28571428571429,-4.68474025750198,1.25527236874723));
#57632=CARTESIAN_POINT('',(6.94805436450009,-5.2439365747499,3.79002385031413E-13));
#57633=CARTESIAN_POINT('Ctrl Pts',(6.94808683301109,-5.24392552271844,1.87509820678312E-5));
#57634=CARTESIAN_POINT('Ctrl Pts',(7.12497029401787,-5.03766626339576,0.3063486516447));
#57635=CARTESIAN_POINT('Ctrl Pts',(7.26874438305119,-4.84340706140497,0.595319568935955));
#57636=CARTESIAN_POINT('Ctrl Pts',(7.38338779618054,-4.65435739713307,0.876016191369865));
#57637=CARTESIAN_POINT('',(7.46165237939775,-4.51772599325679,-1.07877301257371));
#57638=CARTESIAN_POINT('Ctrl Pts',(7.46165237939775,-4.51772599325679,-1.07877301257371));
#57639=CARTESIAN_POINT('Ctrl Pts',(7.33663088231331,-4.7499056562241,-0.734446773842698));
#57640=CARTESIAN_POINT('Ctrl Pts',(7.16787076968654,-4.98766689283078,-0.380608346073431));
#57641=CARTESIAN_POINT('Ctrl Pts',(6.94809164225636,-5.24392405018006,-2.12859752396575E-5));
#57642=CARTESIAN_POINT('',(7.49999999999943,-4.44436879421741,-1.18641730474127));
#57643=CARTESIAN_POINT('Ctrl Pts',(7.50000000105064,-4.44436879327718,-1.18641730372645));
#57644=CARTESIAN_POINT('Ctrl Pts',(7.48748585582718,-4.46904262342706,-1.15059487498792));
#57645=CARTESIAN_POINT('Ctrl Pts',(7.47470152024076,-4.49349219992046,-1.11471212456586));
#57646=CARTESIAN_POINT('Ctrl Pts',(7.46165237939775,-4.51772599325679,-1.07877301257371));
#57647=CARTESIAN_POINT('',(7.49999999999943,1.18641730474065,4.44436879421757));
#57648=CARTESIAN_POINT('Origin',(7.5,0.,0.));
#57649=CARTESIAN_POINT('Ctrl Pts',(7.46165237939758,1.07877301257324,4.51772599325711));
#57650=CARTESIAN_POINT('Ctrl Pts',(7.47470152024065,1.11471212456534,4.49349219992073));
#57651=CARTESIAN_POINT('Ctrl Pts',(7.48748585582712,1.15059487498736,4.46904262342728));
#57652=CARTESIAN_POINT('Ctrl Pts',(7.50000000105064,1.18641730372584,4.44436879327734));
#57653=CARTESIAN_POINT('Ctrl Pts',(7.38338779618106,-0.876016191369523,
4.65435739713289));
#57654=CARTESIAN_POINT('Ctrl Pts',(7.26874438305275,-0.595319568934126,
4.84340706140535));
#57655=CARTESIAN_POINT('Ctrl Pts',(7.12497029402482,-0.306348651646226,
5.03766626339399));
#57656=CARTESIAN_POINT('Ctrl Pts',(6.94808683301396,-1.87509829813626E-5,
5.24392552271746));
#57657=CARTESIAN_POINT('Origin',(1.5,-4.65899107620574,2.68986975199945));
#57658=CARTESIAN_POINT('',(1.6,-4.53548868402095,2.90378217011979));
#57659=CARTESIAN_POINT('',(1.5,-4.53548868402095,2.90378217011979));
#57660=CARTESIAN_POINT('',(1.6,-4.78249346839052,2.4759573338791));
#57661=CARTESIAN_POINT('',(1.6,-4.21524107620573,3.45846729785813));
#57662=CARTESIAN_POINT('',(1.5,-4.78249346839052,2.4759573338791));
#57663=CARTESIAN_POINT('Origin',(1.5,-3.42946788875475,3.42946788875476));
#57664=CARTESIAN_POINT('',(1.6,-3.42946788875475,3.42946788875476));
#57665=CARTESIAN_POINT('',(1.5,-3.42946788875475,3.42946788875476));
#57666=CARTESIAN_POINT('',(1.6,-1.24762653078691,4.46648531837259));
#57667=CARTESIAN_POINT('Origin',(1.5,2.68986975199945,-4.65899107620574));
#57668=CARTESIAN_POINT('',(6.68133955674308,2.68986975199644,-4.65899107620048));
#57669=CARTESIAN_POINT('',(6.4964847157299,2.47595733387918,-4.78249346839053));
#57670=CARTESIAN_POINT('Ctrl Pts',(6.68133955674087,2.6898697519957,-4.65899107619594));
#57671=CARTESIAN_POINT('Ctrl Pts',(6.67492308098284,2.68233846075464,-4.66333926734057));
#57672=CARTESIAN_POINT('Ctrl Pts',(6.6685005684247,2.67481117074313,-4.6676851311398));
#57673=CARTESIAN_POINT('Ctrl Pts',(6.6620720344556,2.66728791952006,-4.67202864152121));
#57674=CARTESIAN_POINT('Ctrl Pts',(6.6073292890923,2.6032230132773,-4.7090161854831));
#57675=CARTESIAN_POINT('Ctrl Pts',(6.55213434648276,2.53943317427306,-4.74584349646418));
#57676=CARTESIAN_POINT('Ctrl Pts',(6.49649612060902,2.47595028107014,-4.78249290359719));
#57677=CARTESIAN_POINT('',(1.6,2.4759573338791,-4.78249346839052));
#57678=CARTESIAN_POINT('',(1.5,2.4759573338791,-4.78249346839052));
#57679=CARTESIAN_POINT('',(1.6,2.90378217011979,-4.53548868402095));
#57680=CARTESIAN_POINT('',(1.6,4.02111975199945,-3.89039353034704));
#57681=CARTESIAN_POINT('',(6.49648471573067,2.90378217011975,-4.53548868402103));
#57682=CARTESIAN_POINT('',(1.5,2.90378217011979,-4.53548868402095));
#57683=CARTESIAN_POINT('Ctrl Pts',(6.49648471573075,2.90378217011979,-4.53548868402095));
#57684=CARTESIAN_POINT('Ctrl Pts',(6.55337396234641,2.83888253293793,-4.5729585070182));
#57685=CARTESIAN_POINT('Ctrl Pts',(6.60979834671137,2.77366106395271,-4.61061413969377));
#57686=CARTESIAN_POINT('Ctrl Pts',(6.67094806990306,2.70205935512119,-4.65195340556208));
#57687=CARTESIAN_POINT('Ctrl Pts',(6.67614580655144,2.69596587438841,-4.65547147830345));
#57688=CARTESIAN_POINT('Ctrl Pts',(6.68133955672777,2.68986975198969,-4.65899107621137));
#57689=CARTESIAN_POINT('Origin',(1.5,1.25527236874722,-4.68474025750198));
#57690=CARTESIAN_POINT('',(6.9730266888256,1.25527236925909,-4.68474025754297));
#57691=CARTESIAN_POINT('Ctrl Pts',(6.97303770557678,1.25526723923358,-4.68473984672734));
#57692=CARTESIAN_POINT('Ctrl Pts',(6.85768162673857,1.63799446828719,-4.71538888116549));
#57693=CARTESIAN_POINT('Ctrl Pts',(6.70189613372097,2.03849703114157,-4.74746137538506));
#57694=CARTESIAN_POINT('Ctrl Pts',(6.49649612060898,2.47595028107023,-4.7824929035972));
#57695=CARTESIAN_POINT('',(1.6,1.25527236874722,-4.68474025750198));
#57696=CARTESIAN_POINT('',(1.5,1.25527236874722,-4.68474025750198));
#57697=CARTESIAN_POINT('',(1.6,2.20894193499413,-4.76111070924851));
#57698=CARTESIAN_POINT('Ctrl Pts',(6.45213506683142,2.5693960002115,-4.78997609487978));
#57699=CARTESIAN_POINT('Ctrl Pts',(6.69496761877087,2.06333956306628,-4.7494507807858));
#57700=CARTESIAN_POINT('Ctrl Pts',(6.87214261929781,1.60732229617945,-4.71293263455469));
#57701=CARTESIAN_POINT('Ctrl Pts',(6.99737260418699,1.17271712435015,-4.67812918220736));
#57702=CARTESIAN_POINT('Ctrl Pts',(6.59045151583296,2.6420974655224,-4.71093147065315));
#57703=CARTESIAN_POINT('Ctrl Pts',(6.83894619948317,2.13090865278461,-4.67186091612313));
#57704=CARTESIAN_POINT('Ctrl Pts',(7.02199092230211,1.6676886040292,-4.63669438947174));
#57705=CARTESIAN_POINT('Ctrl Pts',(7.15213252925719,1.22335080384112,-4.60270344939976));
#57706=CARTESIAN_POINT('Ctrl Pts',(6.7287679648345,2.7147989308333,-4.63188684642652));
#57707=CARTESIAN_POINT('Ctrl Pts',(6.98292478019547,2.19847774250294,-4.59427105146045));
#57708=CARTESIAN_POINT('Ctrl Pts',(7.17183922530641,1.72805491187895,-4.56045614438878));
#57709=CARTESIAN_POINT('Ctrl Pts',(7.30689245432738,1.27398448333209,-4.52727771659216));
#57710=CARTESIAN_POINT('Ctrl Pts',(6.86708441383604,2.78750039614421,-4.5528422221999));
#57711=CARTESIAN_POINT('Ctrl Pts',(7.12690336090777,2.26604683222127,-4.51668118679778));
#57712=CARTESIAN_POINT('Ctrl Pts',(7.32168752831071,1.78842121972871,-4.48421789930582));
#57713=CARTESIAN_POINT('Ctrl Pts',(7.46165237939758,1.32461816282306,-4.45185198378456));
#57714=CARTESIAN_POINT('',(6.94805436450009,2.62196828737462,-4.54138228956796));
#57715=CARTESIAN_POINT('Ctrl Pts',(6.68133955674308,2.68986975199342,-4.65899107619524));
#57716=CARTESIAN_POINT('Ctrl Pts',(6.76807298446522,2.66766517619599,-4.62053162275364));
#57717=CARTESIAN_POINT('Ctrl Pts',(6.85888718065092,2.64454493763045,-4.58048619487531));
#57718=CARTESIAN_POINT('Ctrl Pts',(6.94805436450009,2.62196828737462,-4.54138228956796));
#57719=CARTESIAN_POINT('',(7.46165237939758,1.32461816282306,-4.45185198378456));
#57720=CARTESIAN_POINT('Ctrl Pts',(6.94809164225473,2.62194359089516,-4.54138208596012));
#57721=CARTESIAN_POINT('Ctrl Pts',(7.16787076968256,2.16421694982277,-4.50975040784356));
#57722=CARTESIAN_POINT('Ctrl Pts',(7.33663088231394,1.73890326423272,-4.4807623507912));
#57723=CARTESIAN_POINT('Ctrl Pts',(7.46165237939758,1.32461816282306,-4.45185198378456));
#57724=CARTESIAN_POINT('',(7.17384635845204,1.23045504008019,-4.59212072600841));
#57725=CARTESIAN_POINT('Ctrl Pts',(7.46165237939758,1.32461816282306,-4.45185198378456));
#57726=CARTESIAN_POINT('Ctrl Pts',(7.36571703908244,1.29323045524197,-4.4986082311925));
#57727=CARTESIAN_POINT('Ctrl Pts',(7.26978169876729,1.26184274766089,-4.54536447860044));
#57728=CARTESIAN_POINT('Ctrl Pts',(7.17384635845215,1.2304550400798,-4.59212072600838));
#57729=CARTESIAN_POINT('Ctrl Pts',(6.97302668796278,1.25527236889283,-4.68474025804403));
#57730=CARTESIAN_POINT('Ctrl Pts',(7.04027818843189,1.24693497884552,-4.65362469478567));
#57731=CARTESIAN_POINT('Ctrl Pts',(7.10373004606705,1.23909393123521,-4.62436150671982));
#57732=CARTESIAN_POINT('Ctrl Pts',(7.17384635845204,1.23045504008019,-4.5921207260084));
#57733=CARTESIAN_POINT('Ctrl Pts',(6.99737260418672,3.46502015180142,-3.35466741224479));
#57734=CARTESIAN_POINT('Ctrl Pts',(6.872142618999,3.27785823931047,-3.74844825878233));
#57735=CARTESIAN_POINT('Ctrl Pts',(6.69496761793157,3.08147524771389,-4.16162987061385));
#57736=CARTESIAN_POINT('Ctrl Pts',(6.45213506509495,2.86354298002157,-4.6201502592847));
#57737=CARTESIAN_POINT('Ctrl Pts',(7.15213252925707,3.37438271134571,-3.3608045985668));
#57738=CARTESIAN_POINT('Ctrl Pts',(7.02199092199136,3.18165082839044,-3.76260789239011));
#57739=CARTESIAN_POINT('Ctrl Pts',(6.83894619861566,2.98049590895782,-4.18135148651518));
#57740=CARTESIAN_POINT('Ctrl Pts',(6.59045151405566,2.75873759472565,-4.64358926304999));
#57741=CARTESIAN_POINT('Ctrl Pts',(7.30689245432741,3.28374527089,-3.3669417848888));
#57742=CARTESIAN_POINT('Ctrl Pts',(7.17183922498372,3.08544341747041,-3.77676752599789));
#57743=CARTESIAN_POINT('Ctrl Pts',(6.98292477929974,2.87951657020175,-4.20107310241652));
#57744=CARTESIAN_POINT('Ctrl Pts',(6.72876796301637,2.65393220942972,-4.66702826681527));
#57745=CARTESIAN_POINT('Ctrl Pts',(7.46165237939775,3.1931078304343,-3.37307897121081));
#57746=CARTESIAN_POINT('Ctrl Pts',(7.32168752797609,2.98923600655038,-3.79092715960567));
#57747=CARTESIAN_POINT('Ctrl Pts',(7.12690335998383,2.77853723144567,-4.22079471831786));
#57748=CARTESIAN_POINT('Ctrl Pts',(6.86708441197709,2.54912682413379,-4.69046727058056));
#57749=CARTESIAN_POINT('',(6.9730266888256,3.42946788921854,-3.42946788853432));
#57750=CARTESIAN_POINT('Ctrl Pts',(6.49649612061063,2.9037852073991,-4.53548229371214));
#57751=CARTESIAN_POINT('Ctrl Pts',(6.70189613387517,3.09217363913432,-4.13912090191365));
#57752=CARTESIAN_POINT('Ctrl Pts',(6.85768162696566,3.26464932591708,-3.77623926085462));
#57753=CARTESIAN_POINT('Ctrl Pts',(6.97303770582829,3.42947009812916,-3.42946324032328));
#57754=CARTESIAN_POINT('',(7.17384635845203,3.36166568592825,-3.36166568592823));
#57755=CARTESIAN_POINT('Ctrl Pts',(6.9730266882762,3.42946788904572,-3.42946788904523));
#57756=CARTESIAN_POINT('Ctrl Pts',(7.04024193630111,3.40670199458592,-3.40670199458569));
#57757=CARTESIAN_POINT('Ctrl Pts',(7.10380439458312,3.38524254899082,-3.38524254899074));
#57758=CARTESIAN_POINT('Ctrl Pts',(7.17384635845204,3.36166568592824,-3.36166568592822));
#57759=CARTESIAN_POINT('',(7.46165237939775,3.1931078304343,-3.37307897121081));
#57760=CARTESIAN_POINT('Ctrl Pts',(7.46165237939775,3.1931078304343,-3.37307897121081));
#57761=CARTESIAN_POINT('Ctrl Pts',(7.36571703908251,3.24929378226561,-3.36927454278328));
#57762=CARTESIAN_POINT('Ctrl Pts',(7.26978169876727,3.30547973409693,-3.36547011435575));
#57763=CARTESIAN_POINT('Ctrl Pts',(7.17384635845203,3.36166568592825,-3.36166568592823));
#57764=CARTESIAN_POINT('Ctrl Pts',(7.46165237939775,3.1931078304343,-3.37307897121081));
#57765=CARTESIAN_POINT('Ctrl Pts',(7.33663088231331,3.01100239198735,-3.74631557694812));
#57766=CARTESIAN_POINT('Ctrl Pts',(7.16787076968672,2.82344994300742,-4.12914206176923));
#57767=CARTESIAN_POINT('Ctrl Pts',(6.94809164225641,2.62198045928535,-4.54136079998446));
#57768=CARTESIAN_POINT('Origin',(1.5,4.65899107620573,-2.68986975199945));
#57769=CARTESIAN_POINT('',(6.68133955674308,4.65899107620051,-2.6898697519964));
#57770=CARTESIAN_POINT('',(6.4964847157299,4.53548868402102,-2.90378217011975));
#57771=CARTESIAN_POINT('Ctrl Pts',(6.68133955674087,4.65899107619759,-2.68986975199284));
#57772=CARTESIAN_POINT('Ctrl Pts',(6.67492308098284,4.65464288223185,-2.69740104160513));
#57773=CARTESIAN_POINT('Ctrl Pts',(6.6685005684247,4.65029698975985,-2.7049283150624));
#57774=CARTESIAN_POINT('Ctrl Pts',(6.6620720344556,4.64595341827232,-2.71245153100584));
#57775=CARTESIAN_POINT('Ctrl Pts',(6.6073292890926,4.60896535395617,-2.77651613682146));
#57776=CARTESIAN_POINT('Ctrl Pts',(6.55213434648291,4.57213538836561,-2.84030444318645));
#57777=CARTESIAN_POINT('Ctrl Pts',(6.49649612060902,4.53548229371255,-2.90378520739891));
#57778=CARTESIAN_POINT('',(1.6,4.53548868402095,-2.90378217011979));
#57779=CARTESIAN_POINT('',(1.5,4.53548868402095,-2.90378217011979));
#57780=CARTESIAN_POINT('',(1.6,4.78249346839052,-2.47595733387911));
#57781=CARTESIAN_POINT('',(1.6,5.10274107620574,-1.92127220614076));
#57782=CARTESIAN_POINT('',(6.49648471573067,4.78249346839052,-2.47595733387919));
#57783=CARTESIAN_POINT('',(1.5,4.78249346839052,-2.47595733387911));
#57784=CARTESIAN_POINT('Ctrl Pts',(6.49648471573075,4.78249346839052,-2.4759573338791));
#57785=CARTESIAN_POINT('Ctrl Pts',(6.55337396234637,4.74502364539329,-2.54085697106091));
#57786=CARTESIAN_POINT('Ctrl Pts',(6.60979834671129,4.70736801271776,-2.60607844004609));
#57787=CARTESIAN_POINT('Ctrl Pts',(6.67094806990306,4.66602874684939,-2.6776801488777));
#57788=CARTESIAN_POINT('Ctrl Pts',(6.67614580655144,4.66251067410802,-2.68377362961048));
#57789=CARTESIAN_POINT('Ctrl Pts',(6.68133955672777,4.6589910762001,-2.6898697520092));
#57790=CARTESIAN_POINT('Origin',(1.5,3.42946788875475,-3.42946788875476));
#57791=CARTESIAN_POINT('Ctrl Pts',(6.97303770557678,3.42946324107831,-3.4294700977703));
#57792=CARTESIAN_POINT('Ctrl Pts',(6.85768162673857,3.77623926137783,-3.26464932566841));
#57793=CARTESIAN_POINT('Ctrl Pts',(6.70189613372097,4.13912090220029,-3.09217363899809));
#57794=CARTESIAN_POINT('Ctrl Pts',(6.49649612060898,4.53548229371264,-2.90378520739886));
#57795=CARTESIAN_POINT('',(1.6,3.42946788875475,-3.42946788875476));
#57796=CARTESIAN_POINT('',(1.5,3.42946788875475,-3.42946788875476));
#57797=CARTESIAN_POINT('',(1.6,4.14344644123463,-3.09011773362498));
#57798=CARTESIAN_POINT('Ctrl Pts',(6.45213506683141,4.62015025600519,-2.86354298158031));
#57799=CARTESIAN_POINT('Ctrl Pts',(6.69496761877087,4.1616298686418,-3.0814752486512));
#57800=CARTESIAN_POINT('Ctrl Pts',(6.87214261929781,3.74844825783789,-3.27785823975936));
#57801=CARTESIAN_POINT('Ctrl Pts',(6.99737260418699,3.35466741224394,-3.46502015180182));
#57802=CARTESIAN_POINT('Ctrl Pts',(6.59045151583295,4.64358925974348,-2.758737596312));
#57803=CARTESIAN_POINT('Ctrl Pts',(6.83894619948317,4.18135148451713,-2.98049590991796));
#57804=CARTESIAN_POINT('Ctrl Pts',(7.02199092230211,3.76260789142697,-3.1816508288527));
#57805=CARTESIAN_POINT('Ctrl Pts',(7.15213252925719,3.3608045985664,-3.3743827113459));
#57806=CARTESIAN_POINT('Ctrl Pts',(6.72876796483449,4.66702826348176,-2.6539322110437));
#57807=CARTESIAN_POINT('Ctrl Pts',(6.98292478019547,4.20107310039245,-2.87951657118472));
#57808=CARTESIAN_POINT('Ctrl Pts',(7.17183922530641,3.77676752501605,-3.08544341794604));
#57809=CARTESIAN_POINT('Ctrl Pts',(7.30689245432738,3.36694178488886,-3.28374527088997));
#57810=CARTESIAN_POINT('Ctrl Pts',(6.86708441383603,4.69046726722004,-2.5491268257754));
#57811=CARTESIAN_POINT('Ctrl Pts',(7.12690336090776,4.22079471626778,-2.77853723245148));
#57812=CARTESIAN_POINT('Ctrl Pts',(7.32168752831071,3.79092715860513,-2.98923600703938));
#57813=CARTESIAN_POINT('Ctrl Pts',(7.46165237939758,3.37307897121132,-3.19310783043405));
#57814=CARTESIAN_POINT('',(6.94805436450009,4.54138228956758,-2.62196828737528));
#57815=CARTESIAN_POINT('Ctrl Pts',(6.68133955674308,4.65899107619527,-2.68986975199337));
#57816=CARTESIAN_POINT('Ctrl Pts',(6.76807293638616,4.62053164407291,-2.66766518850469));
#57817=CARTESIAN_POINT('Ctrl Pts',(6.8588871155266,4.58048622343516,-2.64454495411985));
#57818=CARTESIAN_POINT('Ctrl Pts',(6.94805436450009,4.54138228956758,-2.62196828737528));
#57819=CARTESIAN_POINT('',(7.46165237939758,3.37307897121132,-3.19310783043405));
#57820=CARTESIAN_POINT('Ctrl Pts',(6.94809164225473,4.54136079998506,-2.62198045928545));
#57821=CARTESIAN_POINT('Ctrl Pts',(7.16787076968256,4.12914206176917,-2.82344994300837));
#57822=CARTESIAN_POINT('Ctrl Pts',(7.33663088231394,3.74631557694482,-3.0110023919897));
#57823=CARTESIAN_POINT('Ctrl Pts',(7.46165237939758,3.37307897121132,-3.19310783043405));
#57824=CARTESIAN_POINT('Ctrl Pts',(7.46165237939758,3.37307897121132,-3.19310783043405));
#57825=CARTESIAN_POINT('Ctrl Pts',(7.36571703908244,3.36927454278351,-3.2492937822655));
#57826=CARTESIAN_POINT('Ctrl Pts',(7.26978169876729,3.3654701143557,-3.30547973409695));
#57827=CARTESIAN_POINT('Ctrl Pts',(7.17384635845215,3.36166568592789,-3.36166568592839));
#57828=CARTESIAN_POINT('Ctrl Pts',(6.99737260418672,4.67812918220743,-1.17271712435108));
#57829=CARTESIAN_POINT('Ctrl Pts',(6.872142618999,4.71293263463817,-1.60732229722181));
#57830=CARTESIAN_POINT('Ctrl Pts',(6.69496761793157,4.7494507809601,-2.06333956524279));
#57831=CARTESIAN_POINT('Ctrl Pts',(6.45213506509495,4.78997609516963,-2.56939600383103));
#57832=CARTESIAN_POINT('Ctrl Pts',(7.15213252925707,4.6027034493998,-1.22335080384155));
#57833=CARTESIAN_POINT('Ctrl Pts',(7.02199092199136,4.63669438955298,-1.66768860509444));
#57834=CARTESIAN_POINT('Ctrl Pts',(6.83894619861566,4.67186091629066,-2.13090865499507));
#57835=CARTESIAN_POINT('Ctrl Pts',(6.59045151405566,4.71093147093258,-2.64209746917913));
#57836=CARTESIAN_POINT('Ctrl Pts',(7.30689245432741,4.52727771659216,-1.27398448333202));
#57837=CARTESIAN_POINT('Ctrl Pts',(7.17183922498372,4.56045614446779,-1.72805491296707));
#57838=CARTESIAN_POINT('Ctrl Pts',(6.98292477929974,4.59427105162121,-2.19847774474734));
#57839=CARTESIAN_POINT('Ctrl Pts',(6.72876796301638,4.63188684669553,-2.71479893452723));
#57840=CARTESIAN_POINT('Ctrl Pts',(7.46165237939775,4.45185198378452,-1.32461816282249));
#57841=CARTESIAN_POINT('Ctrl Pts',(7.32168752797609,4.48421789938261,-1.7884212208397));
#57842=CARTESIAN_POINT('Ctrl Pts',(7.12690335998383,4.51668118695177,-2.26604683449962));
#57843=CARTESIAN_POINT('Ctrl Pts',(6.86708441197709,4.55284222245849,-2.78750039987533));
#57844=CARTESIAN_POINT('',(6.9730266888256,4.68474025779341,-1.25527236832443));
#57845=CARTESIAN_POINT('Ctrl Pts',(6.49649612061063,4.78249290359715,-2.47595028106968));
#57846=CARTESIAN_POINT('Ctrl Pts',(6.70189613387517,4.74746137535973,-2.03849703082522));
#57847=CARTESIAN_POINT('Ctrl Pts',(6.85768162696566,4.71538888111925,-1.63799446770973));
#57848=CARTESIAN_POINT('Ctrl Pts',(6.97303770582829,4.68473984666061,-1.25526723840028));
#57849=CARTESIAN_POINT('',(7.17384635845204,4.59212072600841,-1.23045504008016));
#57850=CARTESIAN_POINT('Ctrl Pts',(6.9730266882762,4.6847402578992,-1.2552723688533));
#57851=CARTESIAN_POINT('Ctrl Pts',(7.04024207626693,4.65364140296873,-1.24693945578933));
#57852=CARTESIAN_POINT('Ctrl Pts',(7.10380410094938,4.62432745491165,-1.23908480708058));
#57853=CARTESIAN_POINT('Ctrl Pts',(7.17384635845203,4.59212072600842,-1.23045504008016));
#57854=CARTESIAN_POINT('',(7.46165237939775,4.45185198378452,-1.32461816282249));
#57855=CARTESIAN_POINT('Ctrl Pts',(7.46165237939775,4.45185198378452,-1.32461816282249));
#57856=CARTESIAN_POINT('Ctrl Pts',(7.36571703908251,4.49860823119249,-1.29323045524171));
#57857=CARTESIAN_POINT('Ctrl Pts',(7.26978169876728,4.54536447860045,-1.26184274766094));
#57858=CARTESIAN_POINT('Ctrl Pts',(7.17384635845204,4.59212072600841,-1.23045504008016));
#57859=CARTESIAN_POINT('Ctrl Pts',(7.46165237939775,4.45185198378452,-1.32461816282249));
#57860=CARTESIAN_POINT('Ctrl Pts',(7.33663088231331,4.48076235079081,-1.73890326423675));
#57861=CARTESIAN_POINT('Ctrl Pts',(7.16787076968672,4.50975040784277,-2.1642169498233));
#57862=CARTESIAN_POINT('Ctrl Pts',(6.94809164225642,4.54138208595974,-2.62194359089469));
#57863=CARTESIAN_POINT('Origin',(1.5,5.37973950399889,-3.46944695195361E-17));
#57864=CARTESIAN_POINT('',(6.68133955674308,5.37973950399284,2.68350805758692E-14));
#57865=CARTESIAN_POINT('',(6.4964847157299,5.37973950399894,-0.2470047843695));
#57866=CARTESIAN_POINT('Ctrl Pts',(6.68133955674087,5.37973950398853,1.65381597305725E-12));
#57867=CARTESIAN_POINT('Ctrl Pts',(6.67492308098284,5.37973950235977,-0.00869638510872296));
#57868=CARTESIAN_POINT('Ctrl Pts',(6.6685005684247,5.37973948580553,-0.0173881413799512));
#57869=CARTESIAN_POINT('Ctrl Pts',(6.6620720344556,5.3797394505259,-0.0260752232488909));
#57870=CARTESIAN_POINT('Ctrl Pts',(6.6073292890922,5.37973915009911,-0.100050831527283));
#57871=CARTESIAN_POINT('Ctrl Pts',(6.55213434648271,5.37973761745967,-0.173708108098733));
#57872=CARTESIAN_POINT('Ctrl Pts',(6.49649612060902,5.37973548846904,-0.247010609884637));
#57873=CARTESIAN_POINT('',(1.6,5.37973950399889,-0.247004784369567));
#57874=CARTESIAN_POINT('',(1.5,5.37973950399889,-0.247004784369567));
#57875=CARTESIAN_POINT('',(1.6,5.37973950399889,0.247004784369567));
#57876=CARTESIAN_POINT('',(1.6,5.37973950399889,-1.73472347597681E-17));
#57877=CARTESIAN_POINT('',(6.49648471573067,5.37973950399894,0.247004784369499));
#57878=CARTESIAN_POINT('',(1.5,5.37973950399889,0.247004784369567));
#57879=CARTESIAN_POINT('Ctrl Pts',(6.49648471573075,5.37973950399889,0.247004784369566));
#57880=CARTESIAN_POINT('Ctrl Pts',(6.55337396234643,5.37973950399889,0.172065138375048));
#57881=CARTESIAN_POINT('Ctrl Pts',(6.60979834671138,5.37973950399889,0.0967538730239298));
#57882=CARTESIAN_POINT('Ctrl Pts',(6.67094806990306,5.37973950399889,0.0140753412873033));
#57883=CARTESIAN_POINT('Ctrl Pts',(6.67614580655144,5.37973950399889,0.00703919580456445));
#57884=CARTESIAN_POINT('Ctrl Pts',(6.68133955672778,5.37973950399889,-1.12624232856406E-11));
#57885=CARTESIAN_POINT('Origin',(1.5,4.68474025750198,-1.25527236874722));
#57886=CARTESIAN_POINT('Ctrl Pts',(6.97303770557678,4.68473733700388,-1.25527660564903));
#57887=CARTESIAN_POINT('Ctrl Pts',(6.85768162673858,4.90264379395559,-0.939149619787658));
#57888=CARTESIAN_POINT('Ctrl Pts',(6.70189613372098,5.13067067013966,-0.608340473184774));
#57889=CARTESIAN_POINT('Ctrl Pts',(6.49649612060898,5.37973548846909,-0.24701060988456));
#57890=CARTESIAN_POINT('',(1.6,4.68474025750198,-1.25527236874722));
#57891=CARTESIAN_POINT('',(1.5,4.68474025750198,-1.25527236874722));
#57892=CARTESIAN_POINT('',(1.6,4.79527416765606,-1.09491570772261));
#57893=CARTESIAN_POINT('Ctrl Pts',(6.45213506683129,5.43293898179196,-0.169825838874389));
#57894=CARTESIAN_POINT('Ctrl Pts',(6.69496761877082,5.14481481171758,-0.587820912143886));
#57895=CARTESIAN_POINT('Ctrl Pts',(6.8721426192978,4.88518053593885,-0.964484376716747));
#57896=CARTESIAN_POINT('Ctrl Pts',(6.99737260418699,4.63773727615197,-1.32346176996341));
#57897=CARTESIAN_POINT('Ctrl Pts',(6.59045151583283,5.40083506183456,-0.0673422109094779));
#57898=CARTESIAN_POINT('Ctrl Pts',(6.83894619948311,5.11140456270267,-0.490509431605882));
#57899=CARTESIAN_POINT('Ctrl Pts',(7.02199092230209,4.84933943288195,-0.874086498044709));
#57900=CARTESIAN_POINT('Ctrl Pts',(7.15213252925719,4.59773351518701,-1.24189885083336));
#57901=CARTESIAN_POINT('Ctrl Pts',(6.72876796483437,5.36873114187716,0.0351414170554329));
#57902=CARTESIAN_POINT('Ctrl Pts',(6.98292478019541,5.07799431368776,-0.393197951067879));
#57903=CARTESIAN_POINT('Ctrl Pts',(7.17183922530639,4.81349832982504,-0.783688619372671));
#57904=CARTESIAN_POINT('Ctrl Pts',(7.30689245432738,4.55772975422206,-1.1603359317033));
#57905=CARTESIAN_POINT('Ctrl Pts',(6.86708441383591,5.33662722191976,0.137625045020344));
#57906=CARTESIAN_POINT('Ctrl Pts',(7.12690336090771,5.04458406467285,-0.295886470529875));
#57907=CARTESIAN_POINT('Ctrl Pts',(7.32168752831068,4.77765722676813,-0.693290740700633));
#57908=CARTESIAN_POINT('Ctrl Pts',(7.46165237939758,4.51772599325711,-1.07877301257324));
#57909=CARTESIAN_POINT('',(6.94805436450009,5.2439365747499,-3.78100328823905E-13));
#57910=CARTESIAN_POINT('Ctrl Pts',(6.94805436450009,5.2439365747499,-3.77996245415346E-13));
#57911=CARTESIAN_POINT('Ctrl Pts',(6.85888652980287,5.2890902048436,-1.56816092780279E-13));
#57912=CARTESIAN_POINT('Ctrl Pts',(6.76807250396892,5.33533059841515,-3.28976807639418E-15));
#57913=CARTESIAN_POINT('Ctrl Pts',(6.68133955674308,5.37973950398679,2.77382283808691E-14));
#57914=CARTESIAN_POINT('',(7.46165237939758,4.51772599325711,-1.07877301257324));
#57915=CARTESIAN_POINT('Ctrl Pts',(6.94809164225473,5.24392405018061,-2.1285975059784E-5));
#57916=CARTESIAN_POINT('Ctrl Pts',(7.16787076968256,4.98766689283114,-0.380608346074386));
#57917=CARTESIAN_POINT('Ctrl Pts',(7.33663088231394,4.74990565622242,-0.734446773846379));
#57918=CARTESIAN_POINT('Ctrl Pts',(7.46165237939758,4.51772599325711,-1.07877301257324));
#57919=CARTESIAN_POINT('Ctrl Pts',(7.46165237939758,4.51772599325711,-1.07877301257324));
#57920=CARTESIAN_POINT('Ctrl Pts',(7.36571703908244,4.54252423750747,-1.12933368840899));
#57921=CARTESIAN_POINT('Ctrl Pts',(7.26978169876729,4.56732248175783,-1.17989436424473));
#57922=CARTESIAN_POINT('Ctrl Pts',(7.17384635845215,4.59212072600819,-1.23045504008048));
#57923=CARTESIAN_POINT('Origin',(1.5,-5.37973950399889,6.24500451351651E-16));
#57924=CARTESIAN_POINT('',(6.68133955603507,-5.3797395041741,-2.68543263356575E-14));
#57925=CARTESIAN_POINT('',(6.49648471572948,-5.37973950399919,0.247004784369128));
#57926=CARTESIAN_POINT('Ctrl Pts',(6.68133955609892,-5.37973950429881,4.70876809766096E-11));
#57927=CARTESIAN_POINT('Ctrl Pts',(6.67484047849818,-5.37973950253171,0.00880833749040602));
#57928=CARTESIAN_POINT('Ctrl Pts',(6.66833520149437,-5.37973948712148,0.0176119236098385));
#57929=CARTESIAN_POINT('Ctrl Pts',(6.66182374103212,-5.37973945439155,0.0264107107560584));
#57930=CARTESIAN_POINT('Ctrl Pts',(6.60716230063611,-5.3797391796352,0.100273461200274));
#57931=CARTESIAN_POINT('Ctrl Pts',(6.55204961798885,-5.3797377938976,0.173818622858807));
#57932=CARTESIAN_POINT('Ctrl Pts',(6.49649473556378,-5.37973586027059,0.247010070494919));
#57933=CARTESIAN_POINT('',(1.6,-5.37973950399889,0.247004784369568));
#57934=CARTESIAN_POINT('',(1.5,-5.37973950399889,0.247004784369567));
#57935=CARTESIAN_POINT('',(1.6,-5.37973950399889,-0.247004784369566));
#57936=CARTESIAN_POINT('',(1.6,-5.37973950399889,3.12250225675825E-16));
#57937=CARTESIAN_POINT('',(6.49648471573068,-5.37973950399894,-0.247004784369499));
#57938=CARTESIAN_POINT('',(1.5,-5.37973950399889,-0.247004784369566));
#57939=CARTESIAN_POINT('Ctrl Pts',(6.49648471573075,-5.37973950399889,-0.247004784369566));
#57940=CARTESIAN_POINT('Ctrl Pts',(6.55337396234644,-5.37973950399889,-0.172065138375028));
#57941=CARTESIAN_POINT('Ctrl Pts',(6.60979834671144,-5.37973950399889,-0.0967538730238504));
#57942=CARTESIAN_POINT('Ctrl Pts',(6.67094806981975,-5.37973950399889,-0.0140753413999544));
#57943=CARTESIAN_POINT('Ctrl Pts',(6.67614580638494,-5.37973950399889,-0.00703919602996617));
#57944=CARTESIAN_POINT('Ctrl Pts',(6.6813395564782,-5.37973950399889,-3.26986319965084E-10));
#57945=CARTESIAN_POINT('Origin',(1.5,-4.68474025750198,1.25527236874723));
#57946=CARTESIAN_POINT('',(6.97302668913438,-4.68474025750198,1.25527236874723));
#57947=CARTESIAN_POINT('Ctrl Pts',(6.97302668913438,-4.68474025750198,1.25527236874723));
#57948=CARTESIAN_POINT('Ctrl Pts',(6.85757546768185,-4.90267228949946,0.939108279982866));
#57949=CARTESIAN_POINT('Ctrl Pts',(6.70188214814575,-5.1306744242805,0.608335026878845));
#57950=CARTESIAN_POINT('Ctrl Pts',(6.49649473556348,-5.37973586027094,0.247010070494401));
#57951=CARTESIAN_POINT('',(1.6,-4.68474025750198,1.25527236874723));
#57952=CARTESIAN_POINT('',(1.5,-4.68474025750198,1.25527236874723));
#57953=CARTESIAN_POINT('',(1.6,-3.65183350576906,2.75375801561154));
#57954=CARTESIAN_POINT('Ctrl Pts',(6.45213506859891,-5.43293897969466,0.169825841917048));
#57955=CARTESIAN_POINT('Ctrl Pts',(6.67964185096999,-5.16299904623435,0.561440201226003));
#57956=CARTESIAN_POINT('Ctrl Pts',(6.84940428693712,-4.91809665661411,0.916731436483211));
#57957=CARTESIAN_POINT('Ctrl Pts',(6.97302668913438,-4.68474025750198,1.25527236874723));
#57958=CARTESIAN_POINT('Ctrl Pts',(6.59045151764167,-5.40083505972775,0.0673422139897861));
#57959=CARTESIAN_POINT('Ctrl Pts',(6.82326308044043,-5.12967124289664,0.463802293582382));
#57960=CARTESIAN_POINT('Ctrl Pts',(6.99850389520073,-4.88256196744721,0.825458102897624));
#57961=CARTESIAN_POINT('Ctrl Pts',(7.12684466416208,-4.64550450560471,1.17205861623332));
#57962=CARTESIAN_POINT('Ctrl Pts',(6.72876796668442,-5.36873113976084,-0.0351414139374756));
#57963=CARTESIAN_POINT('Ctrl Pts',(6.96688430991087,-5.09634343955894,0.366164385938763));
#57964=CARTESIAN_POINT('Ctrl Pts',(7.14760350346434,-4.84702727828031,0.734184769312034));
#57965=CARTESIAN_POINT('Ctrl Pts',(7.28066263918978,-4.60626875370745,1.08884486371941));
#57966=CARTESIAN_POINT('Ctrl Pts',(6.86708441572717,-5.33662721979393,-0.137625041864737));
#57967=CARTESIAN_POINT('Ctrl Pts',(7.11050553938132,-5.06301563622124,0.268526478295141));
#57968=CARTESIAN_POINT('Ctrl Pts',(7.29670311172796,-4.81149258911341,0.642911435726447));
#57969=CARTESIAN_POINT('Ctrl Pts',(7.43448061421748,-4.56703300181018,1.0056311112055));
#57970=CARTESIAN_POINT('Ctrl Pts',(6.68133955603507,-5.3797395043493,-2.62984078958084E-14));
#57971=CARTESIAN_POINT('Ctrl Pts',(6.77016782808452,-5.33425770985245,1.14024814220434E-7));
#57972=CARTESIAN_POINT('Ctrl Pts',(6.85900408935791,-5.28903269339668,7.30333645709156E-6));
#57973=CARTESIAN_POINT('Ctrl Pts',(6.94808683301108,-5.24392552271845,1.87509820665649E-5));
#57974=CARTESIAN_POINT('Ctrl Pts',(6.97302668913438,-4.68474025750198,1.25527236874723));
#57975=CARTESIAN_POINT('Ctrl Pts',(7.04204931539975,-4.67972462592243,1.1926400929975));
#57976=CARTESIAN_POINT('Ctrl Pts',(7.11079264180597,-4.67468173820311,1.12966745850414));
#57977=CARTESIAN_POINT('Ctrl Pts',(7.24755133540632,-4.66455755467053,1.00324257168837));
#57978=CARTESIAN_POINT('Ctrl Pts',(7.31560085004917,-4.6594738889069,0.939760724810945));
#57979=CARTESIAN_POINT('Ctrl Pts',(7.38335469474695,-4.65436776006777,0.875998372175109));
#57980=CARTESIAN_POINT('Ctrl Pts',(6.99737260418672,-4.6377372761525,-1.32346176996264));
#57981=CARTESIAN_POINT('Ctrl Pts',(6.87214261900943,-4.88518053651166,-0.964484375885747));
#57982=CARTESIAN_POINT('Ctrl Pts',(6.69496761796091,-5.14481481291349,-0.58782091040892));
#57983=CARTESIAN_POINT('Ctrl Pts',(6.45213506515565,-5.43293898378058,-0.169825835989406));
#57984=CARTESIAN_POINT('Ctrl Pts',(7.15213252925706,-4.59773351518726,-1.241898850833));
#57985=CARTESIAN_POINT('Ctrl Pts',(7.0219909220022,-4.84933943346392,-0.874086497193518));
#57986=CARTESIAN_POINT('Ctrl Pts',(6.83894619864596,-5.11140456390929,-0.490509429839278));
#57987=CARTESIAN_POINT('Ctrl Pts',(6.59045151411778,-5.40083506383243,-0.0673422079883656));
#57988=CARTESIAN_POINT('Ctrl Pts',(7.30689245432741,-4.55772975422203,-1.16033593170336));
#57989=CARTESIAN_POINT('Ctrl Pts',(7.17183922499498,-4.81349833041617,-0.783688618501289));
#57990=CARTESIAN_POINT('Ctrl Pts',(6.98292477933101,-5.07799431490509,-0.393197949269635));
#57991=CARTESIAN_POINT('Ctrl Pts',(6.7287679630799,-5.36873114388427,0.035141420012675));
#57992=CARTESIAN_POINT('Ctrl Pts',(7.46165237939775,-4.51772599325679,-1.07877301257371));
#57993=CARTESIAN_POINT('Ctrl Pts',(7.32168752798775,-4.77765722736842,-0.693290739809061));
#57994=CARTESIAN_POINT('Ctrl Pts',(7.12690336001606,-5.04458406590089,-0.295886468699992));
#57995=CARTESIAN_POINT('Ctrl Pts',(6.86708441204203,-5.33662722393612,0.137625048013716));
#57996=CARTESIAN_POINT('',(6.9730266888256,-4.68474025754297,-1.25527236925909));
#57997=CARTESIAN_POINT('Ctrl Pts',(6.49649612061061,-5.37973548846879,-0.247010609885));
#57998=CARTESIAN_POINT('Ctrl Pts',(6.70189613387502,-5.1306706699596,-0.608340473445991));
#57999=CARTESIAN_POINT('Ctrl Pts',(6.85768162696565,-4.90264379362682,-0.939149620264615));
#58000=CARTESIAN_POINT('Ctrl Pts',(6.97303770582828,-4.68473733652944,-1.25527660633732));
#58001=CARTESIAN_POINT('',(7.17384635845204,-4.5921207260084,-1.23045504008019));
#58002=CARTESIAN_POINT('Ctrl Pts',(6.97302668796278,-4.68474025804403,-1.25527236889283));
#58003=CARTESIAN_POINT('Ctrl Pts',(7.04027818843198,-4.65362469478563,-1.24693497884551));
#58004=CARTESIAN_POINT('Ctrl Pts',(7.10373004606737,-4.62436150671968,-1.23909393123517));
#58005=CARTESIAN_POINT('Ctrl Pts',(7.17384635845204,-4.5921207260084,-1.23045504008019));
#58006=CARTESIAN_POINT('Ctrl Pts',(7.46165237939775,-4.51772599325679,-1.07877301257371));
#58007=CARTESIAN_POINT('Ctrl Pts',(7.36571703908252,-4.54252423750733,-1.1293336884092));
#58008=CARTESIAN_POINT('Ctrl Pts',(7.26978169876728,-4.56732248175787,-1.17989436424469));
#58009=CARTESIAN_POINT('Ctrl Pts',(7.17384635845204,-4.5921207260084,-1.23045504008019));
#58010=CARTESIAN_POINT('Origin',(1.5,-4.65899107620574,-2.68986975199945));
#58011=CARTESIAN_POINT('',(6.68133955674308,-4.65899107620048,-2.68986975199644));
#58012=CARTESIAN_POINT('',(6.4964847157299,-4.78249346839053,-2.47595733387918));
#58013=CARTESIAN_POINT('Ctrl Pts',(6.68133955674087,-4.65899107619594,-2.6898697519957));
#58014=CARTESIAN_POINT('Ctrl Pts',(6.67492308098284,-4.66333926734057,-2.68233846075464));
#58015=CARTESIAN_POINT('Ctrl Pts',(6.6685005684247,-4.6676851311398,-2.67481117074314));
#58016=CARTESIAN_POINT('Ctrl Pts',(6.6620720344556,-4.67202864152121,-2.66728791952006));
#58017=CARTESIAN_POINT('Ctrl Pts',(6.60732928909247,-4.70901618548299,-2.60322301327749));
#58018=CARTESIAN_POINT('Ctrl Pts',(6.55213434648284,-4.74584349646412,-2.53943317427315));
#58019=CARTESIAN_POINT('Ctrl Pts',(6.49649612060902,-4.78249290359719,-2.47595028107014));
#58020=CARTESIAN_POINT('',(1.6,-4.78249346839052,-2.4759573338791));
#58021=CARTESIAN_POINT('',(1.5,-4.78249346839052,-2.4759573338791));
#58022=CARTESIAN_POINT('',(1.6,-4.53548868402095,-2.90378217011979));
#58023=CARTESIAN_POINT('',(1.6,-4.21524107620573,-3.45846729785814));
#58024=CARTESIAN_POINT('',(6.49648471573068,-4.53548868402103,-2.90378217011975));
#58025=CARTESIAN_POINT('',(1.5,-4.53548868402095,-2.90378217011979));
#58026=CARTESIAN_POINT('Ctrl Pts',(6.49648471573075,-4.53548868402095,-2.90378217011979));
#58027=CARTESIAN_POINT('Ctrl Pts',(6.55337396234641,-4.5729585070182,-2.83888253293794));
#58028=CARTESIAN_POINT('Ctrl Pts',(6.60979834671136,-4.61061413969376,-2.77366106395272));
#58029=CARTESIAN_POINT('Ctrl Pts',(6.67094806990306,-4.65195340556208,-2.70205935512119));
#58030=CARTESIAN_POINT('Ctrl Pts',(6.67614580655144,-4.65547147830345,-2.69596587438841));
#58031=CARTESIAN_POINT('Ctrl Pts',(6.68133955672777,-4.65899107621137,-2.68986975198969));
#58032=CARTESIAN_POINT('Origin',(1.5,-4.68474025750198,-1.25527236874723));
#58033=CARTESIAN_POINT('Ctrl Pts',(6.97303770557678,-4.68473984672734,-1.25526723923358));
#58034=CARTESIAN_POINT('Ctrl Pts',(6.85768162673857,-4.71538888116549,-1.63799446828719));
#58035=CARTESIAN_POINT('Ctrl Pts',(6.70189613372097,-4.74746137538506,-2.03849703114157));
#58036=CARTESIAN_POINT('Ctrl Pts',(6.49649612060898,-4.7824929035972,-2.47595028107023));
#58037=CARTESIAN_POINT('',(1.6,-4.68474025750198,-1.25527236874723));
#58038=CARTESIAN_POINT('',(1.5,-4.68474025750198,-1.25527236874723));
#58039=CARTESIAN_POINT('',(1.6,-4.6085629719582,-0.304014949143111));
#58040=CARTESIAN_POINT('Ctrl Pts',(6.45213506683142,-4.78997609487978,-2.5693960002115));
#58041=CARTESIAN_POINT('Ctrl Pts',(6.69496761877088,-4.74945078078581,-2.06333956306629));
#58042=CARTESIAN_POINT('Ctrl Pts',(6.87214261929782,-4.71293263455469,-1.60732229617945));
#58043=CARTESIAN_POINT('Ctrl Pts',(6.99737260418699,-4.67812918220736,-1.17271712435015));
#58044=CARTESIAN_POINT('Ctrl Pts',(6.59045151583296,-4.71093147065315,-2.6420974655224));
#58045=CARTESIAN_POINT('Ctrl Pts',(6.83894619948317,-4.67186091612313,-2.13090865278462));
#58046=CARTESIAN_POINT('Ctrl Pts',(7.02199092230211,-4.63669438947174,-1.6676886040292));
#58047=CARTESIAN_POINT('Ctrl Pts',(7.15213252925719,-4.60270344939976,-1.22335080384112));
#58048=CARTESIAN_POINT('Ctrl Pts',(6.7287679648345,-4.63188684642652,-2.7147989308333));
#58049=CARTESIAN_POINT('Ctrl Pts',(6.98292478019547,-4.59427105146045,-2.19847774250294));
#58050=CARTESIAN_POINT('Ctrl Pts',(7.17183922530641,-4.56045614438878,-1.72805491187896));
#58051=CARTESIAN_POINT('Ctrl Pts',(7.30689245432738,-4.52727771659216,-1.27398448333209));
#58052=CARTESIAN_POINT('Ctrl Pts',(6.86708441383604,-4.5528422221999,-2.78750039614421));
#58053=CARTESIAN_POINT('Ctrl Pts',(7.12690336090777,-4.51668118679778,-2.26604683222127));
#58054=CARTESIAN_POINT('Ctrl Pts',(7.32168752831071,-4.48421789930582,-1.78842121972871));
#58055=CARTESIAN_POINT('Ctrl Pts',(7.46165237939758,-4.45185198378456,-1.32461816282306));
#58056=CARTESIAN_POINT('',(6.94805436450009,-4.54138228956795,-2.62196828737462));
#58057=CARTESIAN_POINT('Ctrl Pts',(6.68133955674307,-4.65899107619524,-2.68986975199342));
#58058=CARTESIAN_POINT('Ctrl Pts',(6.76807298446519,-4.62053162275365,-2.66766517619599));
#58059=CARTESIAN_POINT('Ctrl Pts',(6.85888718065087,-4.58048619487533,-2.64454493763046));
#58060=CARTESIAN_POINT('Ctrl Pts',(6.94805436450009,-4.54138228956796,-2.62196828737462));
#58061=CARTESIAN_POINT('',(7.46165237939758,-4.45185198378456,-1.32461816282306));
#58062=CARTESIAN_POINT('Ctrl Pts',(6.94809164225473,-4.54138208596012,-2.62194359089516));
#58063=CARTESIAN_POINT('Ctrl Pts',(7.16787076968256,-4.50975040784356,-2.16421694982278));
#58064=CARTESIAN_POINT('Ctrl Pts',(7.33663088231394,-4.4807623507912,-1.73890326423272));
#58065=CARTESIAN_POINT('Ctrl Pts',(7.46165237939758,-4.45185198378456,-1.32461816282306));
#58066=CARTESIAN_POINT('Ctrl Pts',(7.46165237939758,-4.45185198378456,-1.32461816282306));
#58067=CARTESIAN_POINT('Ctrl Pts',(7.36571703908244,-4.4986082311925,-1.29323045524197));
#58068=CARTESIAN_POINT('Ctrl Pts',(7.2697816987673,-4.54536447860044,-1.26184274766089));
#58069=CARTESIAN_POINT('Ctrl Pts',(7.17384635845216,-4.59212072600837,-1.2304550400798));
#58070=CARTESIAN_POINT('Ctrl Pts',(6.99737260418672,-3.35466741224479,-3.46502015180142));
#58071=CARTESIAN_POINT('Ctrl Pts',(6.872142618999,-3.74844825878233,-3.27785823931047));
#58072=CARTESIAN_POINT('Ctrl Pts',(6.69496761793157,-4.16162987061385,-3.08147524771389));
#58073=CARTESIAN_POINT('Ctrl Pts',(6.45213506509495,-4.6201502592847,-2.86354298002157));
#58074=CARTESIAN_POINT('Ctrl Pts',(7.15213252925707,-3.3608045985668,-3.37438271134571));
#58075=CARTESIAN_POINT('Ctrl Pts',(7.02199092199136,-3.76260789239011,-3.18165082839044));
#58076=CARTESIAN_POINT('Ctrl Pts',(6.83894619861565,-4.18135148651518,-2.98049590895782));
#58077=CARTESIAN_POINT('Ctrl Pts',(6.59045151405566,-4.64358926304999,-2.75873759472565));
#58078=CARTESIAN_POINT('Ctrl Pts',(7.30689245432741,-3.3669417848888,-3.28374527089));
#58079=CARTESIAN_POINT('Ctrl Pts',(7.17183922498372,-3.77676752599789,-3.08544341747041));
#58080=CARTESIAN_POINT('Ctrl Pts',(6.98292477929974,-4.20107310241652,-2.87951657020175));
#58081=CARTESIAN_POINT('Ctrl Pts',(6.72876796301637,-4.66702826681527,-2.65393220942972));
#58082=CARTESIAN_POINT('Ctrl Pts',(7.46165237939775,-3.37307897121081,-3.1931078304343));
#58083=CARTESIAN_POINT('Ctrl Pts',(7.32168752797609,-3.79092715960566,-2.98923600655038));
#58084=CARTESIAN_POINT('Ctrl Pts',(7.12690335998383,-4.22079471831786,-2.77853723144567));
#58085=CARTESIAN_POINT('Ctrl Pts',(6.86708441197709,-4.69046727058056,-2.54912682413379));
#58086=CARTESIAN_POINT('',(6.9730266888256,-3.42946788853432,-3.42946788921854));
#58087=CARTESIAN_POINT('Ctrl Pts',(6.49649612061063,-4.53548229371214,-2.9037852073991));
#58088=CARTESIAN_POINT('Ctrl Pts',(6.70189613387517,-4.13912090191365,-3.09217363913432));
#58089=CARTESIAN_POINT('Ctrl Pts',(6.85768162696566,-3.77623926085462,-3.26464932591708));
#58090=CARTESIAN_POINT('Ctrl Pts',(6.97303770582829,-3.42946324032328,-3.42947009812916));
#58091=CARTESIAN_POINT('',(7.17384635845204,-3.36166568592822,-3.36166568592824));
#58092=CARTESIAN_POINT('Ctrl Pts',(6.9730266882762,-3.42946788904522,-3.42946788904572));
#58093=CARTESIAN_POINT('Ctrl Pts',(7.04024193630125,-3.40670199458563,-3.40670199458587));
#58094=CARTESIAN_POINT('Ctrl Pts',(7.10380439458351,-3.3852425489906,-3.38524254899069));
#58095=CARTESIAN_POINT('Ctrl Pts',(7.17384635845203,-3.36166568592823,-3.36166568592825));
#58096=CARTESIAN_POINT('',(7.46165237939775,-3.37307897121081,-3.1931078304343));
#58097=CARTESIAN_POINT('Ctrl Pts',(7.46165237939775,-3.37307897121081,-3.1931078304343));
#58098=CARTESIAN_POINT('Ctrl Pts',(7.36571703908251,-3.36927454278328,-3.24929378226561));
#58099=CARTESIAN_POINT('Ctrl Pts',(7.26978169876727,-3.36547011435575,-3.30547973409693));
#58100=CARTESIAN_POINT('Ctrl Pts',(7.17384635845203,-3.36166568592822,-3.36166568592824));
#58101=CARTESIAN_POINT('Ctrl Pts',(7.46165237939775,-3.37307897121081,-3.1931078304343));
#58102=CARTESIAN_POINT('Ctrl Pts',(7.33663088231331,-3.74631557694812,-3.01100239198735));
#58103=CARTESIAN_POINT('Ctrl Pts',(7.16787076968672,-4.12914206176923,-2.82344994300742));
#58104=CARTESIAN_POINT('Ctrl Pts',(6.94809164225641,-4.54136079998446,-2.62198045928535));
#58105=CARTESIAN_POINT('Origin',(1.5,-2.68986975199945,-4.65899107620573));
#58106=CARTESIAN_POINT('',(6.68133955674308,-2.6898697519964,-4.65899107620051));
#58107=CARTESIAN_POINT('',(6.4964847157299,-2.90378217011975,-4.53548868402102));
#58108=CARTESIAN_POINT('Ctrl Pts',(6.68133955674087,-2.68986975199284,-4.65899107619759));
#58109=CARTESIAN_POINT('Ctrl Pts',(6.67492308098284,-2.69740104160513,-4.65464288223185));
#58110=CARTESIAN_POINT('Ctrl Pts',(6.6685005684247,-2.7049283150624,-4.65029698975985));
#58111=CARTESIAN_POINT('Ctrl Pts',(6.6620720344556,-2.71245153100584,-4.64595341827232));
#58112=CARTESIAN_POINT('Ctrl Pts',(6.6073292890925,-2.77651613682158,-4.6089653539561));
#58113=CARTESIAN_POINT('Ctrl Pts',(6.55213434648286,-2.8403044431865,-4.57213538836558));
#58114=CARTESIAN_POINT('Ctrl Pts',(6.49649612060902,-2.9037852073989,-4.53548229371255));
#58115=CARTESIAN_POINT('',(1.6,-2.90378217011979,-4.53548868402095));
#58116=CARTESIAN_POINT('',(1.5,-2.90378217011979,-4.53548868402095));
#58117=CARTESIAN_POINT('',(1.6,-2.47595733387911,-4.78249346839052));
#58118=CARTESIAN_POINT('',(1.6,-1.35861975199945,-5.42758862206442));
#58119=CARTESIAN_POINT('',(6.49648471573067,-2.47595733387919,-4.78249346839052));
#58120=CARTESIAN_POINT('',(1.5,-2.47595733387911,-4.78249346839052));
#58121=CARTESIAN_POINT('Ctrl Pts',(6.49648471573075,-2.4759573338791,-4.78249346839052));
#58122=CARTESIAN_POINT('Ctrl Pts',(6.55337396234636,-2.5408569710609,-4.7450236453933));
#58123=CARTESIAN_POINT('Ctrl Pts',(6.60979834671127,-2.60607844004607,-4.70736801271777));
#58124=CARTESIAN_POINT('Ctrl Pts',(6.67094806990306,-2.6776801488777,-4.66602874684939));
#58125=CARTESIAN_POINT('Ctrl Pts',(6.67614580655144,-2.68377362961048,-4.66251067410802));
#58126=CARTESIAN_POINT('Ctrl Pts',(6.68133955672777,-2.6898697520092,-4.6589910762001));
#58127=CARTESIAN_POINT('Origin',(1.5,-3.42946788875476,-3.42946788875475));
#58128=CARTESIAN_POINT('Ctrl Pts',(6.97303770557678,-3.4294700977703,-3.42946324107831));
#58129=CARTESIAN_POINT('Ctrl Pts',(6.85768162673857,-3.26464932566841,-3.77623926137783));
#58130=CARTESIAN_POINT('Ctrl Pts',(6.70189613372097,-3.09217363899809,-4.13912090220029));
#58131=CARTESIAN_POINT('Ctrl Pts',(6.49649612060898,-2.90378520739886,-4.53548229371264));
#58132=CARTESIAN_POINT('',(1.6,-3.42946788875476,-3.42946788875475));
#58133=CARTESIAN_POINT('',(1.5,-3.42946788875476,-3.42946788875475));
#58134=CARTESIAN_POINT('',(1.6,-3.45121148122265,-3.38372027838457));
#58135=CARTESIAN_POINT('Ctrl Pts',(6.4521350668314,-2.86354298158031,-4.62015025600519));
#58136=CARTESIAN_POINT('Ctrl Pts',(6.69496761877087,-3.0814752486512,-4.1616298686418));
#58137=CARTESIAN_POINT('Ctrl Pts',(6.87214261929781,-3.27785823975936,-3.74844825783789));
#58138=CARTESIAN_POINT('Ctrl Pts',(6.99737260418699,-3.46502015180182,-3.35466741224394));
#58139=CARTESIAN_POINT('Ctrl Pts',(6.59045151583295,-2.758737596312,-4.64358925974348));
#58140=CARTESIAN_POINT('Ctrl Pts',(6.83894619948317,-2.98049590991796,-4.18135148451713));
#58141=CARTESIAN_POINT('Ctrl Pts',(7.02199092230211,-3.1816508288527,-3.76260789142697));
#58142=CARTESIAN_POINT('Ctrl Pts',(7.15213252925719,-3.3743827113459,-3.3608045985664));
#58143=CARTESIAN_POINT('Ctrl Pts',(6.72876796483449,-2.6539322110437,-4.66702826348176));
#58144=CARTESIAN_POINT('Ctrl Pts',(6.98292478019547,-2.87951657118472,-4.20107310039245));
#58145=CARTESIAN_POINT('Ctrl Pts',(7.17183922530641,-3.08544341794604,-3.77676752501605));
#58146=CARTESIAN_POINT('Ctrl Pts',(7.30689245432738,-3.28374527088997,-3.36694178488886));
#58147=CARTESIAN_POINT('Ctrl Pts',(6.86708441383603,-2.54912682577539,-4.69046726722004));
#58148=CARTESIAN_POINT('Ctrl Pts',(7.12690336090776,-2.77853723245148,-4.22079471626778));
#58149=CARTESIAN_POINT('Ctrl Pts',(7.3216875283107,-2.98923600703938,-3.79092715860513));
#58150=CARTESIAN_POINT('Ctrl Pts',(7.46165237939758,-3.19310783043405,-3.37307897121132));
#58151=CARTESIAN_POINT('',(6.94805436450009,-2.62196828737528,-4.54138228956758));
#58152=CARTESIAN_POINT('Ctrl Pts',(6.68133955674308,-2.68986975199337,-4.65899107619527));
#58153=CARTESIAN_POINT('Ctrl Pts',(6.76807293638611,-2.6676651885047,-4.62053164407294));
#58154=CARTESIAN_POINT('Ctrl Pts',(6.85888711552652,-2.64454495411987,-4.5804862234352));
#58155=CARTESIAN_POINT('Ctrl Pts',(6.94805436450009,-2.62196828737528,-4.54138228956758));
#58156=CARTESIAN_POINT('',(7.46165237939758,-3.19310783043405,-3.37307897121132));
#58157=CARTESIAN_POINT('Ctrl Pts',(6.94809164225473,-2.62198045928545,-4.54136079998506));
#58158=CARTESIAN_POINT('Ctrl Pts',(7.16787076968256,-2.82344994300837,-4.12914206176917));
#58159=CARTESIAN_POINT('Ctrl Pts',(7.33663088231394,-3.0110023919897,-3.74631557694482));
#58160=CARTESIAN_POINT('Ctrl Pts',(7.46165237939758,-3.19310783043405,-3.37307897121132));
#58161=CARTESIAN_POINT('Ctrl Pts',(7.46165237939758,-3.19310783043405,-3.37307897121132));
#58162=CARTESIAN_POINT('Ctrl Pts',(7.36571703908244,-3.2492937822655,-3.36927454278351));
#58163=CARTESIAN_POINT('Ctrl Pts',(7.26978169876729,-3.30547973409695,-3.3654701143557));
#58164=CARTESIAN_POINT('Ctrl Pts',(7.17384635845215,-3.36166568592839,-3.36166568592789));
#58165=CARTESIAN_POINT('Ctrl Pts',(6.99737260418672,-1.17271712435108,-4.67812918220743));
#58166=CARTESIAN_POINT('Ctrl Pts',(6.872142618999,-1.60732229722181,-4.71293263463817));
#58167=CARTESIAN_POINT('Ctrl Pts',(6.69496761793157,-2.06333956524279,-4.7494507809601));
#58168=CARTESIAN_POINT('Ctrl Pts',(6.45213506509495,-2.56939600383103,-4.78997609516963));
#58169=CARTESIAN_POINT('Ctrl Pts',(7.15213252925706,-1.22335080384155,-4.6027034493998));
#58170=CARTESIAN_POINT('Ctrl Pts',(7.02199092199136,-1.66768860509444,-4.63669438955298));
#58171=CARTESIAN_POINT('Ctrl Pts',(6.83894619861566,-2.13090865499507,-4.67186091629066));
#58172=CARTESIAN_POINT('Ctrl Pts',(6.59045151405566,-2.64209746917913,-4.71093147093258));
#58173=CARTESIAN_POINT('Ctrl Pts',(7.30689245432741,-1.27398448333202,-4.52727771659216));
#58174=CARTESIAN_POINT('Ctrl Pts',(7.17183922498372,-1.72805491296707,-4.56045614446779));
#58175=CARTESIAN_POINT('Ctrl Pts',(6.98292477929975,-2.19847774474734,-4.59427105162121));
#58176=CARTESIAN_POINT('Ctrl Pts',(6.72876796301638,-2.71479893452723,-4.63188684669553));
#58177=CARTESIAN_POINT('Ctrl Pts',(7.46165237939775,-1.32461816282249,-4.45185198378452));
#58178=CARTESIAN_POINT('Ctrl Pts',(7.32168752797609,-1.7884212208397,-4.48421789938261));
#58179=CARTESIAN_POINT('Ctrl Pts',(7.12690335998383,-2.26604683449962,-4.51668118695177));
#58180=CARTESIAN_POINT('Ctrl Pts',(6.86708441197709,-2.78750039987533,-4.55284222245849));
#58181=CARTESIAN_POINT('',(6.9730266888256,-1.25527236832443,-4.68474025779341));
#58182=CARTESIAN_POINT('Ctrl Pts',(6.49649612061064,-2.47595028106968,-4.78249290359715));
#58183=CARTESIAN_POINT('Ctrl Pts',(6.70189613387518,-2.03849703082522,-4.74746137535973));
#58184=CARTESIAN_POINT('Ctrl Pts',(6.85768162696566,-1.63799446770973,-4.71538888111925));
#58185=CARTESIAN_POINT('Ctrl Pts',(6.97303770582829,-1.25526723840028,-4.68473984666061));
#58186=CARTESIAN_POINT('',(7.17384635845203,-1.23045504008016,-4.59212072600842));
#58187=CARTESIAN_POINT('Ctrl Pts',(6.9730266882762,-1.2552723688533,-4.6847402578992));
#58188=CARTESIAN_POINT('Ctrl Pts',(7.04024207626698,-1.24693945578933,-4.65364140296871));
#58189=CARTESIAN_POINT('Ctrl Pts',(7.10380410094959,-1.23908480708055,-4.62432745491155));
#58190=CARTESIAN_POINT('Ctrl Pts',(7.17384635845203,-1.23045504008016,-4.59212072600842));
#58191=CARTESIAN_POINT('',(7.46165237939775,-1.32461816282249,-4.45185198378452));
#58192=CARTESIAN_POINT('Ctrl Pts',(7.46165237939775,-1.32461816282249,-4.45185198378452));
#58193=CARTESIAN_POINT('Ctrl Pts',(7.36571703908251,-1.29323045524171,-4.49860823119249));
#58194=CARTESIAN_POINT('Ctrl Pts',(7.26978169876727,-1.26184274766094,-4.54536447860045));
#58195=CARTESIAN_POINT('Ctrl Pts',(7.17384635845203,-1.23045504008016,-4.59212072600842));
#58196=CARTESIAN_POINT('Ctrl Pts',(7.46165237939775,-1.32461816282249,-4.45185198378452));
#58197=CARTESIAN_POINT('Ctrl Pts',(7.33663088231331,-1.73890326423675,-4.48076235079082));
#58198=CARTESIAN_POINT('Ctrl Pts',(7.16787076968672,-2.1642169498233,-4.50975040784277));
#58199=CARTESIAN_POINT('Ctrl Pts',(6.94809164225641,-2.62194359089469,-4.54138208595974));
#58200=CARTESIAN_POINT('Origin',(1.5,-4.33680868994202E-16,-5.37973950399889));
#58201=CARTESIAN_POINT('',(6.68133955674307,2.69770838383767E-14,-5.37973950399284));
#58202=CARTESIAN_POINT('',(6.4964847157299,-0.247004784369499,-5.37973950399894));
#58203=CARTESIAN_POINT('Ctrl Pts',(6.68133955674087,1.65339963942301E-12,
-5.37973950398854));
#58204=CARTESIAN_POINT('Ctrl Pts',(6.67492308098284,-0.00869638510872275,
-5.37973950235977));
#58205=CARTESIAN_POINT('Ctrl Pts',(6.6685005684247,-0.0173881413799495,
-5.37973948580553));
#58206=CARTESIAN_POINT('Ctrl Pts',(6.6620720344556,-0.026075223248889,-5.3797394505259));
#58207=CARTESIAN_POINT('Ctrl Pts',(6.6073292890925,-0.100050831526873,-5.37973915009911));
#58208=CARTESIAN_POINT('Ctrl Pts',(6.55213434648286,-0.173708108098531,
-5.37973761745967));
#58209=CARTESIAN_POINT('Ctrl Pts',(6.49649612060902,-0.247010609884638,
-5.37973548846904));
#58210=CARTESIAN_POINT('',(1.6,-0.247004784369567,-5.37973950399889));
#58211=CARTESIAN_POINT('',(1.5,-0.247004784369567,-5.37973950399889));
#58212=CARTESIAN_POINT('',(1.6,0.247004784369567,-5.37973950399889));
#58213=CARTESIAN_POINT('',(1.6,1.77500000000001,-5.37973950399889));
#58214=CARTESIAN_POINT('',(6.49648471573067,0.2470047843695,-5.37973950399894));
#58215=CARTESIAN_POINT('',(1.5,0.247004784369566,-5.37973950399889));
#58216=CARTESIAN_POINT('Ctrl Pts',(6.49648471573075,0.247004784369566,-5.37973950399889));
#58217=CARTESIAN_POINT('Ctrl Pts',(6.55337396234641,0.17206513837507,-5.37973950399889));
#58218=CARTESIAN_POINT('Ctrl Pts',(6.60979834671137,0.096753873023939,-5.37973950399889));
#58219=CARTESIAN_POINT('Ctrl Pts',(6.67094806990306,0.014075341287303,-5.37973950399889));
#58220=CARTESIAN_POINT('Ctrl Pts',(6.67614580655144,0.00703919580456425,
-5.37973950399889));
#58221=CARTESIAN_POINT('Ctrl Pts',(6.68133955672777,-1.12616947017807E-11,
-5.37973950399889));
#58222=CARTESIAN_POINT('Origin',(1.5,-1.25527236874722,-4.68474025750198));
#58223=CARTESIAN_POINT('Ctrl Pts',(6.97303770557678,-1.25527660564903,-4.68473733700388));
#58224=CARTESIAN_POINT('Ctrl Pts',(6.85768162673857,-0.939149619787657,
-4.90264379395559));
#58225=CARTESIAN_POINT('Ctrl Pts',(6.70189613372097,-0.608340473184771,
-5.13067067013966));
#58226=CARTESIAN_POINT('Ctrl Pts',(6.49649612060898,-0.247010609884559,
-5.37973548846909));
#58227=CARTESIAN_POINT('',(1.6,-1.25527236874722,-4.68474025750198));
#58228=CARTESIAN_POINT('',(1.5,-1.25527236874722,-4.68474025750198));
#58229=CARTESIAN_POINT('',(1.6,-0.721057192610576,-5.05297499065702));
#58230=CARTESIAN_POINT('Ctrl Pts',(6.45213506683129,-0.169825838874386,
-5.43293898179197));
#58231=CARTESIAN_POINT('Ctrl Pts',(6.69496761877081,-0.587820912143882,
-5.14481481171758));
#58232=CARTESIAN_POINT('Ctrl Pts',(6.87214261929779,-0.964484376716746,
-4.88518053593886));
#58233=CARTESIAN_POINT('Ctrl Pts',(6.99737260418699,-1.32346176996341,-4.63773727615197));
#58234=CARTESIAN_POINT('Ctrl Pts',(6.59045151583283,-0.0673422109094755,
-5.40083506183456));
#58235=CARTESIAN_POINT('Ctrl Pts',(6.83894619948311,-0.490509431605879,
-5.11140456270267));
#58236=CARTESIAN_POINT('Ctrl Pts',(7.02199092230209,-0.874086498044708,
-4.84933943288195));
#58237=CARTESIAN_POINT('Ctrl Pts',(7.15213252925719,-1.24189885083336,-4.59773351518701));
#58238=CARTESIAN_POINT('Ctrl Pts',(6.72876796483437,0.0351414170554353,
-5.36873114187716));
#58239=CARTESIAN_POINT('Ctrl Pts',(6.98292478019541,-0.393197951067876,
-5.07799431368776));
#58240=CARTESIAN_POINT('Ctrl Pts',(7.17183922530639,-0.783688619372669,
-4.81349832982504));
#58241=CARTESIAN_POINT('Ctrl Pts',(7.30689245432738,-1.1603359317033,-4.55772975422206));
#58242=CARTESIAN_POINT('Ctrl Pts',(6.86708441383591,0.137625045020346,-5.33662722191976));
#58243=CARTESIAN_POINT('Ctrl Pts',(7.1269033609077,-0.295886470529872,-5.04458406467285));
#58244=CARTESIAN_POINT('Ctrl Pts',(7.32168752831068,-0.693290740700631,
-4.77765722676813));
#58245=CARTESIAN_POINT('Ctrl Pts',(7.46165237939758,-1.07877301257324,-4.51772599325711));
#58246=CARTESIAN_POINT('',(6.94805436450009,-3.784472735191E-13,-5.2439365747499));
#58247=CARTESIAN_POINT('Ctrl Pts',(6.68133955674307,2.77425651895591E-14,
-5.37973950398679));
#58248=CARTESIAN_POINT('Ctrl Pts',(6.76807250396894,-2.90644853604443E-15,
-5.33533059841514));
#58249=CARTESIAN_POINT('Ctrl Pts',(6.85888652980292,-1.57039519055847E-13,
-5.28909020484357));
#58250=CARTESIAN_POINT('Ctrl Pts',(6.94805436450009,-3.78239106701983E-13,
-5.2439365747499));
#58251=CARTESIAN_POINT('',(7.46165237939758,-1.07877301257324,-4.51772599325711));
#58252=CARTESIAN_POINT('Ctrl Pts',(6.94809164225473,-2.12859750598534E-5,
-5.24392405018061));
#58253=CARTESIAN_POINT('Ctrl Pts',(7.16787076968256,-0.380608346074385,
-4.98766689283114));
#58254=CARTESIAN_POINT('Ctrl Pts',(7.33663088231394,-0.734446773846379,
-4.74990565622242));
#58255=CARTESIAN_POINT('Ctrl Pts',(7.46165237939758,-1.07877301257324,-4.51772599325711));
#58256=CARTESIAN_POINT('Ctrl Pts',(7.46165237939758,-1.07877301257324,-4.51772599325711));
#58257=CARTESIAN_POINT('Ctrl Pts',(7.36571703908244,-1.12933368840899,-4.54252423750747));
#58258=CARTESIAN_POINT('Ctrl Pts',(7.26978169876729,-1.17989436424473,-4.56732248175783));
#58259=CARTESIAN_POINT('Ctrl Pts',(7.17384635845214,-1.23045504008048,-4.5921207260082));
#58260=CARTESIAN_POINT('Ctrl Pts',(6.99737260418672,1.32346176996264,-4.6377372761525));
#58261=CARTESIAN_POINT('Ctrl Pts',(6.872142618999,0.964484375855836,-4.88518053653228));
#58262=CARTESIAN_POINT('Ctrl Pts',(6.69496761793157,0.587820910346253,-5.14481481295668));
#58263=CARTESIAN_POINT('Ctrl Pts',(6.45213506509495,0.169825835884926,-5.4329389838526));
#58264=CARTESIAN_POINT('Ctrl Pts',(7.15213252925707,1.241898850833,-4.59773351518726));
#58265=CARTESIAN_POINT('Ctrl Pts',(7.02199092199136,0.874086497162872,-4.84933943348488));
#58266=CARTESIAN_POINT('Ctrl Pts',(6.83894619861566,0.49050942977547,-5.11140456395288));
#58267=CARTESIAN_POINT('Ctrl Pts',(6.59045151405566,0.067342207882593,-5.40083506390477));
#58268=CARTESIAN_POINT('Ctrl Pts',(7.30689245432741,1.16033593170335,-4.55772975422203));
#58269=CARTESIAN_POINT('Ctrl Pts',(7.17183922498372,0.783688618469905,-4.81349833043748));
#58270=CARTESIAN_POINT('Ctrl Pts',(6.98292477929975,0.393197949204688,-5.07799431494909));
#58271=CARTESIAN_POINT('Ctrl Pts',(6.72876796301638,-0.0351414201197403,
-5.36873114395694));
#58272=CARTESIAN_POINT('Ctrl Pts',(7.46165237939775,1.07877301257371,-4.51772599325679));
#58273=CARTESIAN_POINT('Ctrl Pts',(7.32168752797609,0.693290739776941,-4.77765722739008));
#58274=CARTESIAN_POINT('Ctrl Pts',(7.12690335998383,0.295886468633904,-5.04458406594529));
#58275=CARTESIAN_POINT('Ctrl Pts',(6.86708441197709,-0.137625048122074,
-5.33662722400912));
#58276=CARTESIAN_POINT('Ctrl Pts',(6.49649612061064,0.247010609885015,-5.37973548846878));
#58277=CARTESIAN_POINT('Ctrl Pts',(6.70189613387518,0.608340473446072,-5.13067066995954));
#58278=CARTESIAN_POINT('Ctrl Pts',(6.85768162696567,0.939149620264625,-4.90264379362682));
#58279=CARTESIAN_POINT('Ctrl Pts',(6.97303770582829,1.25527660633732,-4.68473733652944));
#58280=CARTESIAN_POINT('',(7.46165237939775,1.07877301257371,-4.51772599325679));
#58281=CARTESIAN_POINT('Ctrl Pts',(7.46165237939775,1.07877301257371,-4.51772599325679));
#58282=CARTESIAN_POINT('Ctrl Pts',(7.36571703908251,1.1293336884092,-4.54252423750733));
#58283=CARTESIAN_POINT('Ctrl Pts',(7.26978169876728,1.17989436424469,-4.56732248175787));
#58284=CARTESIAN_POINT('Ctrl Pts',(7.17384635845204,1.23045504008019,-4.59212072600841));
#58285=CARTESIAN_POINT('Ctrl Pts',(7.46165237939775,1.07877301257371,-4.51772599325679));
#58286=CARTESIAN_POINT('Ctrl Pts',(7.33663088231331,0.734446773842696,-4.7499056562241));
#58287=CARTESIAN_POINT('Ctrl Pts',(7.16787076968672,0.380608346073537,-4.98766689283072));
#58288=CARTESIAN_POINT('Ctrl Pts',(6.94809164225642,2.12859752740831E-5,
-5.24392405018004));
#58289=CARTESIAN_POINT('Ctrl Pts',(7.17384635845215,4.5921207260082,-1.23045504008048));
#58290=CARTESIAN_POINT('Ctrl Pts',(7.18694338462328,4.56684952841756,-1.26742353917928));
#58291=CARTESIAN_POINT('Ctrl Pts',(7.1999334636683,4.5414911822982,-1.30436927548241));
#58292=CARTESIAN_POINT('Ctrl Pts',(7.21281435373034,4.51604216132286,-1.3412906003674));
#58293=CARTESIAN_POINT('Ctrl Pts',(7.26978169876729,4.56732248175783,-1.17989436424473));
#58294=CARTESIAN_POINT('Ctrl Pts',(7.28299669995037,4.54214834917584,-1.2168886144726));
#58295=CARTESIAN_POINT('Ctrl Pts',(7.29604661499973,4.5168396920471,-1.25384772750637));
#58296=CARTESIAN_POINT('Ctrl Pts',(7.30892798333169,4.4913910670488,-1.29076915849307));
#58297=CARTESIAN_POINT('Ctrl Pts',(7.36571703908244,4.54252423750747,-1.12933368840899));
#58298=CARTESIAN_POINT('Ctrl Pts',(7.37905001527745,4.51744716993412,-1.16635368976592));
#58299=CARTESIAN_POINT('Ctrl Pts',(7.39215976633117,4.49218820179599,-1.20332617953033));
#58300=CARTESIAN_POINT('Ctrl Pts',(7.40504161293303,4.46673997277473,-1.24024771661874));
#58301=CARTESIAN_POINT('Ctrl Pts',(7.46165237939758,4.51772599325711,-1.07877301257324));
#58302=CARTESIAN_POINT('Ctrl Pts',(7.47510333060454,4.49274599069239,-1.11581876505924));
#58303=CARTESIAN_POINT('Ctrl Pts',(7.4882729176626,4.46753671154489,-1.15280463155429));
#58304=CARTESIAN_POINT('Ctrl Pts',(7.50115524253438,4.44208887850067,-1.18972627474441));
#58305=CARTESIAN_POINT('',(7.49999999999943,4.44436879421757,-1.18641730474065));
#58306=CARTESIAN_POINT('Ctrl Pts',(7.46165237939758,4.51772599325711,-1.07877301257324));
#58307=CARTESIAN_POINT('Ctrl Pts',(7.47470152024065,4.49349219992073,-1.11471212456534));
#58308=CARTESIAN_POINT('Ctrl Pts',(7.48748585582712,4.46904262342728,-1.15059487498735));
#58309=CARTESIAN_POINT('Ctrl Pts',(7.50000000105064,4.44436879327734,-1.18641730372583));
#58310=CARTESIAN_POINT('',(7.49999999999233,4.44238517355639,-1.19033351972209));
#58311=CARTESIAN_POINT('Ctrl Pts',(7.50000000105118,4.44436879327628,-1.18641730372738));
#58312=CARTESIAN_POINT('Ctrl Pts',(7.50000000037148,4.4437079306274,-1.18772277427295));
#58313=CARTESIAN_POINT('Ctrl Pts',(7.49999999647595,4.44304672983401,-1.18902817040918));
#58314=CARTESIAN_POINT('Ctrl Pts',(7.49999999999096,4.44238517355376,-1.19033351972076));
#58315=CARTESIAN_POINT('Ctrl Pts',(7.17384635845215,4.5921207260082,-1.23045504008048));
#58316=CARTESIAN_POINT('Ctrl Pts',(7.19420569065385,4.58275691773915,-1.22794601521635));
#58317=CARTESIAN_POINT('Ctrl Pts',(7.21511409889777,4.57315172570485,-1.22537230751382));
#58318=CARTESIAN_POINT('Ctrl Pts',(7.23681946879609,4.56318819945531,-1.22270258210925));
#58319=CARTESIAN_POINT('Ctrl Pts',(7.32484115407359,4.52278315794258,-1.2118760571323));
#58320=CARTESIAN_POINT('Ctrl Pts',(7.41251895869389,4.48265795751599,-1.20112457966125));
#58321=CARTESIAN_POINT('Ctrl Pts',(7.49999999999091,4.44238517355351,-1.19033351972131));
#58322=CARTESIAN_POINT('Ctrl Pts',(7.17384635845215,3.36166568592789,-3.3616656859284));
#58323=CARTESIAN_POINT('Ctrl Pts',(7.18694338462328,3.32129593728095,-3.38104574649242));
#58324=CARTESIAN_POINT('Ctrl Pts',(7.1999334636683,3.28086209719206,-3.40036251963277));
#58325=CARTESIAN_POINT('Ctrl Pts',(7.21281435373034,3.24036193608348,-3.41961281443688));
#58326=CARTESIAN_POINT('Ctrl Pts',(7.26978169876729,3.3654701143557,-3.30547973409695));
#58327=CARTESIAN_POINT('Ctrl Pts',(7.28299669995037,3.32517155090753,-3.32493062829724));
#58328=CARTESIAN_POINT('Ctrl Pts',(7.29604661499973,3.28477405438148,-3.34428383052146));
#58329=CARTESIAN_POINT('Ctrl Pts',(7.30892798333169,3.24427418314822,-3.36353441520086));
#58330=CARTESIAN_POINT('Ctrl Pts',(7.36571703908244,3.36927454278351,-3.2492937822655));
#58331=CARTESIAN_POINT('Ctrl Pts',(7.37905001527745,3.3290471645341,-3.26881551010206));
#58332=CARTESIAN_POINT('Ctrl Pts',(7.39215976633117,3.2886860115709,-3.28820514141014));
#58333=CARTESIAN_POINT('Ctrl Pts',(7.40504161293303,3.24818643021297,-3.30745601596484));
#58334=CARTESIAN_POINT('Ctrl Pts',(7.46165237939758,3.37307897121132,-3.19310783043405));
#58335=CARTESIAN_POINT('Ctrl Pts',(7.47510333060454,3.33292277816068,-3.21270039190688));
#58336=CARTESIAN_POINT('Ctrl Pts',(7.4882729176626,3.29259796876032,-3.23212645229882));
#58337=CARTESIAN_POINT('Ctrl Pts',(7.50115524253438,3.25209867727771,-3.25137761672882));
#58338=CARTESIAN_POINT('',(7.49999999999943,3.25572762720891,-3.24965192250366));
#58339=CARTESIAN_POINT('Ctrl Pts',(7.46165237939758,3.37307897121132,-3.19310783043405));
#58340=CARTESIAN_POINT('Ctrl Pts',(7.47470152024065,3.3341223345559,-3.21211511774048));
#58341=CARTESIAN_POINT('Ctrl Pts',(7.48748585582712,3.2950070049898,-3.23096570291687));
#58342=CARTESIAN_POINT('Ctrl Pts',(7.50000000105064,3.25572762690205,-3.24965192115468));
#58343=CARTESIAN_POINT('',(7.49999999999233,3.25205165383413,-3.25205165383366));
#58344=CARTESIAN_POINT('Ctrl Pts',(7.50000000105118,3.25572762690036,-3.24965192115549));
#58345=CARTESIAN_POINT('Ctrl Pts',(7.50000000037148,3.25450256807911,-3.25045206029546));
#58346=CARTESIAN_POINT('Ctrl Pts',(7.49999999647522,3.25327725332823,-3.25125196611448));
#58347=CARTESIAN_POINT('Ctrl Pts',(7.49999999999096,3.25205165383252,-3.2520516538312));
#58348=CARTESIAN_POINT('Ctrl Pts',(7.17384635845215,3.36166568592789,-3.36166568592839));
#58349=CARTESIAN_POINT('Ctrl Pts',(7.19420493717887,3.35481115621029,-3.35481115621029));
#58350=CARTESIAN_POINT('Ctrl Pts',(7.21511249441196,3.3477799556656,-3.34777994985528));
#58351=CARTESIAN_POINT('Ctrl Pts',(7.23681685935962,3.34048648878989,-3.34048647397502));
#58352=CARTESIAN_POINT('Ctrl Pts',(7.32483941486432,3.31090766469447,-3.31090761336144));
#58353=CARTESIAN_POINT('Ctrl Pts',(7.41251809600273,3.28153366858765,-3.28153366858751));
#58354=CARTESIAN_POINT('Ctrl Pts',(7.49999999999091,3.25205165383202,-3.25205165383156));
#58355=CARTESIAN_POINT('Ctrl Pts',(7.17384635845215,1.2304550400798,-4.59212072600838));
#58356=CARTESIAN_POINT('Ctrl Pts',(7.18694338462328,1.18580378192515,-4.58871947646023));
#58357=CARTESIAN_POINT('Ctrl Pts',(7.1999334636683,1.14112866266543,-4.58523137267447));
#58358=CARTESIAN_POINT('Ctrl Pts',(7.21281435373034,1.09642934688599,-4.58165253645088));
#58359=CARTESIAN_POINT('Ctrl Pts',(7.26978169876729,1.26184274766089,-4.54536447860044));
#58360=CARTESIAN_POINT('Ctrl Pts',(7.28299669995037,1.21721772087861,-4.54206016538013));
#58361=CARTESIAN_POINT('Ctrl Pts',(7.29604661499973,1.17255586152565,-4.53862178188785));
#58362=CARTESIAN_POINT('Ctrl Pts',(7.30892798333169,1.12785665184795,-4.53504334164129));
#58363=CARTESIAN_POINT('Ctrl Pts',(7.36571703908244,1.29323045524197,-4.4986082311925));
#58364=CARTESIAN_POINT('Ctrl Pts',(7.37905001527745,1.24863165983206,-4.49540085430002));
#58365=CARTESIAN_POINT('Ctrl Pts',(7.39215976633117,1.20398306038586,-4.49201219110123));
#58366=CARTESIAN_POINT('Ctrl Pts',(7.40504161293303,1.15928395680991,-4.4884341468317));
#58367=CARTESIAN_POINT('Ctrl Pts',(7.46165237939758,1.32461816282306,-4.45185198378456));
#58368=CARTESIAN_POINT('Ctrl Pts',(7.47510333060454,1.28004559878552,-4.44874154321992));
#58369=CARTESIAN_POINT('Ctrl Pts',(7.4882729176626,1.23541025924608,-4.44540260031461));
#58370=CARTESIAN_POINT('Ctrl Pts',(7.50115524253438,1.19071126177187,-4.44182495202211));
#58371=CARTESIAN_POINT('',(7.49999999999943,1.19471687171392,-4.44214493194956));
#58372=CARTESIAN_POINT('Ctrl Pts',(7.46165237939758,1.32461816282306,-4.45185198378456));
#58373=CARTESIAN_POINT('Ctrl Pts',(7.47470152024064,1.28137708218025,-4.44883445912125));
#58374=CARTESIAN_POINT('Ctrl Pts',(7.48748585582712,1.23807692051041,-4.44560187997715));
#58375=CARTESIAN_POINT('Ctrl Pts',(7.50000000105064,1.19471687212266,-4.44214493062788));
#58376=CARTESIAN_POINT('',(7.49999999999226,1.19033351972273,-4.44238517355628));
#58377=CARTESIAN_POINT('Ctrl Pts',(7.50000000105118,1.19471687212079,-4.44214493062773));
#58378=CARTESIAN_POINT('Ctrl Pts',(7.50000000037148,1.19325587076909,-4.44222534202356));
#58379=CARTESIAN_POINT('Ctrl Pts',(7.49999999647456,1.19179476415888,-4.4423054234084));
#58380=CARTESIAN_POINT('Ctrl Pts',(7.49999999999088,1.19033351972257,-4.44238517355332));
#58381=CARTESIAN_POINT('Ctrl Pts',(7.17384635845215,1.2304550400798,-4.59212072600838));
#58382=CARTESIAN_POINT('Ctrl Pts',(7.1943969563607,1.22792244418713,-4.58266894946054));
#58383=CARTESIAN_POINT('Ctrl Pts',(7.21552165468888,1.22532214675418,-4.57296449112453));
#58384=CARTESIAN_POINT('Ctrl Pts',(7.23748292043925,1.22262099986246,-4.56288364865534));
#58385=CARTESIAN_POINT('Ctrl Pts',(7.32528335544088,1.21182190135913,-4.52258076429347));
#58386=CARTESIAN_POINT('Ctrl Pts',(7.41273830259814,1.20109752290511,-4.48255698032661));
#58387=CARTESIAN_POINT('Ctrl Pts',(7.49999999999083,1.19033351972196,-4.44238517355338));
#58388=CARTESIAN_POINT('Ctrl Pts',(7.17384635845214,-1.23045504008048,-4.5921207260082));
#58389=CARTESIAN_POINT('Ctrl Pts',(7.18694338462328,-1.26742353917928,-4.56684952841756));
#58390=CARTESIAN_POINT('Ctrl Pts',(7.1999334636683,-1.30436927548242,-4.5414911822982));
#58391=CARTESIAN_POINT('Ctrl Pts',(7.21281435373034,-1.3412906003674,-4.51604216132286));
#58392=CARTESIAN_POINT('Ctrl Pts',(7.26978169876729,-1.17989436424474,-4.56732248175783));
#58393=CARTESIAN_POINT('Ctrl Pts',(7.28299669995036,-1.2168886144726,-4.54214834917584));
#58394=CARTESIAN_POINT('Ctrl Pts',(7.29604661499973,-1.25384772750638,-4.5168396920471));
#58395=CARTESIAN_POINT('Ctrl Pts',(7.30892798333169,-1.29076915849307,-4.4913910670488));
#58396=CARTESIAN_POINT('Ctrl Pts',(7.36571703908244,-1.12933368840899,-4.54252423750747));
#58397=CARTESIAN_POINT('Ctrl Pts',(7.37905001527745,-1.16635368976592,-4.51744716993412));
#58398=CARTESIAN_POINT('Ctrl Pts',(7.39215976633117,-1.20332617953033,-4.49218820179599));
#58399=CARTESIAN_POINT('Ctrl Pts',(7.40504161293303,-1.24024771661874,-4.46673997277473));
#58400=CARTESIAN_POINT('Ctrl Pts',(7.46165237939758,-1.07877301257324,-4.51772599325711));
#58401=CARTESIAN_POINT('Ctrl Pts',(7.47510333060454,-1.11581876505924,-4.49274599069239));
#58402=CARTESIAN_POINT('Ctrl Pts',(7.4882729176626,-1.15280463155429,-4.46753671154489));
#58403=CARTESIAN_POINT('Ctrl Pts',(7.50115524253438,-1.18972627474441,-4.44208887850067));
#58404=CARTESIAN_POINT('',(7.49999999999943,-1.18641730474065,-4.44436879421757));
#58405=CARTESIAN_POINT('Ctrl Pts',(7.46165237939758,-1.07877301257324,-4.51772599325711));
#58406=CARTESIAN_POINT('Ctrl Pts',(7.47470152024065,-1.11471212456534,-4.49349219992073));
#58407=CARTESIAN_POINT('Ctrl Pts',(7.48748585582712,-1.15059487498735,-4.46904262342728));
#58408=CARTESIAN_POINT('Ctrl Pts',(7.50000000105064,-1.18641730372583,-4.44436879327734));
#58409=CARTESIAN_POINT('',(7.49999999999234,-1.19033351972209,-4.44238517355638));
#58410=CARTESIAN_POINT('Ctrl Pts',(7.50000000105118,-1.18641730372738,-4.44436879327628));
#58411=CARTESIAN_POINT('Ctrl Pts',(7.50000000037148,-1.18772277427295,-4.4437079306274));
#58412=CARTESIAN_POINT('Ctrl Pts',(7.49999999647595,-1.18902817040918,-4.44304672983401));
#58413=CARTESIAN_POINT('Ctrl Pts',(7.49999999999097,-1.19033351972076,-4.44238517355376));
#58414=CARTESIAN_POINT('Ctrl Pts',(7.17384635845214,-1.23045504008048,-4.5921207260082));
#58415=CARTESIAN_POINT('Ctrl Pts',(7.19420569065388,-1.22794601521634,-4.58275691773914));
#58416=CARTESIAN_POINT('Ctrl Pts',(7.2151140988978,-1.22537230751381,-4.57315172570483));
#58417=CARTESIAN_POINT('Ctrl Pts',(7.23681946879609,-1.22270258210925,-4.56318819945531));
#58418=CARTESIAN_POINT('Ctrl Pts',(7.32484115407349,-1.21187605713231,-4.52278315794262));
#58419=CARTESIAN_POINT('Ctrl Pts',(7.41251895869389,-1.20112457966125,-4.48265795751599));
#58420=CARTESIAN_POINT('Ctrl Pts',(7.49999999999091,-1.19033351972132,-4.44238517355351));
#58421=CARTESIAN_POINT('Ctrl Pts',(7.17384635845214,-3.3616656859284,-3.36166568592789));
#58422=CARTESIAN_POINT('Ctrl Pts',(7.18694338462328,-3.38104574649242,-3.32129593728095));
#58423=CARTESIAN_POINT('Ctrl Pts',(7.1999334636683,-3.40036251963277,-3.28086209719206));
#58424=CARTESIAN_POINT('Ctrl Pts',(7.21281435373034,-3.41961281443688,-3.24036193608348));
#58425=CARTESIAN_POINT('Ctrl Pts',(7.26978169876729,-3.30547973409695,-3.3654701143557));
#58426=CARTESIAN_POINT('Ctrl Pts',(7.28299669995036,-3.32493062829724,-3.32517155090753));
#58427=CARTESIAN_POINT('Ctrl Pts',(7.29604661499973,-3.34428383052145,-3.28477405438148));
#58428=CARTESIAN_POINT('Ctrl Pts',(7.30892798333169,-3.36353441520086,-3.24427418314822));
#58429=CARTESIAN_POINT('Ctrl Pts',(7.36571703908244,-3.2492937822655,-3.36927454278351));
#58430=CARTESIAN_POINT('Ctrl Pts',(7.37905001527745,-3.26881551010206,-3.3290471645341));
#58431=CARTESIAN_POINT('Ctrl Pts',(7.39215976633117,-3.28820514141014,-3.2886860115709));
#58432=CARTESIAN_POINT('Ctrl Pts',(7.40504161293303,-3.30745601596484,-3.24818643021296));
#58433=CARTESIAN_POINT('Ctrl Pts',(7.46165237939758,-3.19310783043405,-3.37307897121132));
#58434=CARTESIAN_POINT('Ctrl Pts',(7.47510333060454,-3.21270039190688,-3.33292277816068));
#58435=CARTESIAN_POINT('Ctrl Pts',(7.4882729176626,-3.23212645229882,-3.29259796876032));
#58436=CARTESIAN_POINT('Ctrl Pts',(7.50115524253438,-3.25137761672881,-3.25209867727771));
#58437=CARTESIAN_POINT('',(7.49999999999943,-3.24965192250366,-3.25572762720891));
#58438=CARTESIAN_POINT('Ctrl Pts',(7.46165237939758,-3.19310783043405,-3.37307897121132));
#58439=CARTESIAN_POINT('Ctrl Pts',(7.47470152024064,-3.21211511774048,-3.3341223345559));
#58440=CARTESIAN_POINT('Ctrl Pts',(7.48748585582712,-3.23096570291687,-3.2950070049898));
#58441=CARTESIAN_POINT('Ctrl Pts',(7.50000000105064,-3.24965192115468,-3.25572762690205));
#58442=CARTESIAN_POINT('',(7.49999999999234,-3.25205165383366,-3.25205165383413));
#58443=CARTESIAN_POINT('Ctrl Pts',(7.50000000105118,-3.24965192115548,-3.25572762690036));
#58444=CARTESIAN_POINT('Ctrl Pts',(7.50000000037147,-3.25045206029546,-3.25450256807912));
#58445=CARTESIAN_POINT('Ctrl Pts',(7.49999999647523,-3.25125196611448,-3.25327725332823));
#58446=CARTESIAN_POINT('Ctrl Pts',(7.49999999999097,-3.2520516538312,-3.25205165383252));
#58447=CARTESIAN_POINT('Ctrl Pts',(7.17384635845214,-3.3616656859284,-3.36166568592789));
#58448=CARTESIAN_POINT('Ctrl Pts',(7.19420493717891,-3.35481115621028,-3.35481115621027));
#58449=CARTESIAN_POINT('Ctrl Pts',(7.21511249441201,-3.34777994985527,-3.34777995566559));
#58450=CARTESIAN_POINT('Ctrl Pts',(7.23681685935962,-3.34048647397502,-3.34048648878989));
#58451=CARTESIAN_POINT('Ctrl Pts',(7.32483941486278,-3.31090761336196,-3.31090766469499));
#58452=CARTESIAN_POINT('Ctrl Pts',(7.41251809600317,-3.28153366858737,-3.28153366858751));
#58453=CARTESIAN_POINT('Ctrl Pts',(7.49999999999092,-3.25205165383156,-3.25205165383202));
#58454=CARTESIAN_POINT('Ctrl Pts',(7.17384635845215,-4.59212072600837,-1.2304550400798));
#58455=CARTESIAN_POINT('Ctrl Pts',(7.18694338462328,-4.58871947646023,-1.18580378192515));
#58456=CARTESIAN_POINT('Ctrl Pts',(7.19993346366831,-4.58523137267447,-1.14112866266544));
#58457=CARTESIAN_POINT('Ctrl Pts',(7.21281435373035,-4.58165253645087,-1.096429346886));
#58458=CARTESIAN_POINT('Ctrl Pts',(7.2697816987673,-4.54536447860044,-1.26184274766089));
#58459=CARTESIAN_POINT('Ctrl Pts',(7.28299669995037,-4.54206016538012,-1.21721772087861));
#58460=CARTESIAN_POINT('Ctrl Pts',(7.29604661499974,-4.53862178188785,-1.17255586152565));
#58461=CARTESIAN_POINT('Ctrl Pts',(7.30892798333169,-4.53504334164129,-1.12785665184795));
#58462=CARTESIAN_POINT('Ctrl Pts',(7.36571703908244,-4.4986082311925,-1.29323045524197));
#58463=CARTESIAN_POINT('Ctrl Pts',(7.37905001527745,-4.49540085430002,-1.24863165983206));
#58464=CARTESIAN_POINT('Ctrl Pts',(7.39215976633117,-4.49201219110123,-1.20398306038586));
#58465=CARTESIAN_POINT('Ctrl Pts',(7.40504161293303,-4.4884341468317,-1.15928395680991));
#58466=CARTESIAN_POINT('Ctrl Pts',(7.46165237939758,-4.45185198378456,-1.32461816282306));
#58467=CARTESIAN_POINT('Ctrl Pts',(7.47510333060454,-4.44874154321992,-1.28004559878552));
#58468=CARTESIAN_POINT('Ctrl Pts',(7.4882729176626,-4.44540260031461,-1.23541025924608));
#58469=CARTESIAN_POINT('Ctrl Pts',(7.50115524253438,-4.44182495202211,-1.19071126177187));
#58470=CARTESIAN_POINT('',(7.49999999999943,-4.44214493194956,-1.19471687171392));
#58471=CARTESIAN_POINT('Ctrl Pts',(7.46165237939758,-4.45185198378456,-1.32461816282306));
#58472=CARTESIAN_POINT('Ctrl Pts',(7.47470152024065,-4.44883445912125,-1.28137708218025));
#58473=CARTESIAN_POINT('Ctrl Pts',(7.48748585582712,-4.44560187997715,-1.23807692051041));
#58474=CARTESIAN_POINT('Ctrl Pts',(7.50000000105064,-4.44214493062789,-1.19471687212266));
#58475=CARTESIAN_POINT('',(7.49999999999226,-4.44238517355628,-1.19033351972274));
#58476=CARTESIAN_POINT('Ctrl Pts',(7.50000000105118,-4.44214493062774,-1.19471687212079));
#58477=CARTESIAN_POINT('Ctrl Pts',(7.50000000037148,-4.44222534202356,-1.1932558707691));
#58478=CARTESIAN_POINT('Ctrl Pts',(7.49999999647456,-4.4423054234084,-1.19179476415889));
#58479=CARTESIAN_POINT('Ctrl Pts',(7.49999999999088,-4.44238517355332,-1.19033351972258));
#58480=CARTESIAN_POINT('Ctrl Pts',(7.17384635845216,-4.59212072600837,-1.2304550400798));
#58481=CARTESIAN_POINT('Ctrl Pts',(7.19439695636075,-4.58266894946052,-1.22792244418713));
#58482=CARTESIAN_POINT('Ctrl Pts',(7.21552165468893,-4.57296449112451,-1.22532214675418));
#58483=CARTESIAN_POINT('Ctrl Pts',(7.23748292043925,-4.56288364865534,-1.22262099986246));
#58484=CARTESIAN_POINT('Ctrl Pts',(7.32528335544047,-4.52258076429365,-1.21182190135918));
#58485=CARTESIAN_POINT('Ctrl Pts',(7.41273830259824,-4.48255698032657,-1.2010975229051));
#58486=CARTESIAN_POINT('Ctrl Pts',(7.49999999999083,-4.44238517355338,-1.19033351972196));
#58487=CARTESIAN_POINT('Ctrl Pts',(6.99737260418672,4.6377372761525,1.32346176996264));
#58488=CARTESIAN_POINT('Ctrl Pts',(6.872142618999,4.88518053653228,0.964484375855836));
#58489=CARTESIAN_POINT('Ctrl Pts',(6.69496761793157,5.14481481295669,0.587820910346251));
#58490=CARTESIAN_POINT('Ctrl Pts',(6.45213506509495,5.4329389838526,0.169825835884927));
#58491=CARTESIAN_POINT('Ctrl Pts',(7.15213252925707,4.59773351518726,1.241898850833));
#58492=CARTESIAN_POINT('Ctrl Pts',(7.02199092199136,4.84933943348488,0.874086497162871));
#58493=CARTESIAN_POINT('Ctrl Pts',(6.83894619861566,5.11140456395289,0.490509429775467));
#58494=CARTESIAN_POINT('Ctrl Pts',(6.59045151405566,5.40083506390477,0.0673422078825931));
#58495=CARTESIAN_POINT('Ctrl Pts',(7.30689245432741,4.55772975422203,1.16033593170335));
#58496=CARTESIAN_POINT('Ctrl Pts',(7.17183922498372,4.81349833043748,0.783688618469907));
#58497=CARTESIAN_POINT('Ctrl Pts',(6.98292477929974,5.07799431494909,0.393197949204684));
#58498=CARTESIAN_POINT('Ctrl Pts',(6.72876796301638,5.36873114395694,-0.0351414201197404));
#58499=CARTESIAN_POINT('Ctrl Pts',(7.46165237939775,4.51772599325679,1.07877301257371));
#58500=CARTESIAN_POINT('Ctrl Pts',(7.32168752797609,4.77765722739008,0.693290739776942));
#58501=CARTESIAN_POINT('Ctrl Pts',(7.12690335998383,5.04458406594529,0.295886468633901));
#58502=CARTESIAN_POINT('Ctrl Pts',(6.86708441197709,5.33662722400912,-0.137625048122074));
#58503=CARTESIAN_POINT('Ctrl Pts',(6.49649612061064,5.37973548846878,0.247010609885015));
#58504=CARTESIAN_POINT('Ctrl Pts',(6.70189613387518,5.13067066995955,0.608340473446071));
#58505=CARTESIAN_POINT('Ctrl Pts',(6.85768162696567,4.90264379362682,0.939149620264626));
#58506=CARTESIAN_POINT('Ctrl Pts',(6.97303770582829,4.68473733652944,1.25527660633733));
#58507=CARTESIAN_POINT('',(7.46165237939775,4.51772599325679,1.07877301257371));
#58508=CARTESIAN_POINT('Ctrl Pts',(7.46165237939775,4.51772599325679,1.07877301257371));
#58509=CARTESIAN_POINT('Ctrl Pts',(7.36571703908279,4.54252423750726,1.12933368840906));
#58510=CARTESIAN_POINT('Ctrl Pts',(7.26978169876783,4.56732248175773,1.1798943642444));
#58511=CARTESIAN_POINT('Ctrl Pts',(7.17384635845286,4.59212072600819,1.23045504007975));
#58512=CARTESIAN_POINT('Ctrl Pts',(7.46165237939775,4.51772599325679,1.07877301257371));
#58513=CARTESIAN_POINT('Ctrl Pts',(7.33663088231331,4.7499056562241,0.734446773842698));
#58514=CARTESIAN_POINT('Ctrl Pts',(7.16787076968672,4.98766689283072,0.380608346073535));
#58515=CARTESIAN_POINT('Ctrl Pts',(6.94809164225642,5.24392405018004,2.12859752745428E-5));
#58516=CARTESIAN_POINT('Ctrl Pts',(7.17384635845268,4.59212072600811,1.23045504007998));
#58517=CARTESIAN_POINT('Ctrl Pts',(7.18694338462382,4.58871947645997,1.18580378192533));
#58518=CARTESIAN_POINT('Ctrl Pts',(7.19993346366884,4.58523137267421,1.14112866266561));
#58519=CARTESIAN_POINT('Ctrl Pts',(7.21281435373088,4.58165253645062,1.09642934688617));
#58520=CARTESIAN_POINT('Ctrl Pts',(7.26978169876765,4.54536447860026,1.261842747661));
#58521=CARTESIAN_POINT('Ctrl Pts',(7.28299669995072,4.54206016537995,1.21721772087872));
#58522=CARTESIAN_POINT('Ctrl Pts',(7.29604661500009,4.53862178188768,1.17255586152576));
#58523=CARTESIAN_POINT('Ctrl Pts',(7.30892798333205,4.53504334164112,1.12785665184807));
#58524=CARTESIAN_POINT('Ctrl Pts',(7.36571703908262,4.49860823119241,1.29323045524203));
#58525=CARTESIAN_POINT('Ctrl Pts',(7.37905001527763,4.49540085429993,1.24863165983212));
#58526=CARTESIAN_POINT('Ctrl Pts',(7.39215976633134,4.49201219110115,1.20398306038592));
#58527=CARTESIAN_POINT('Ctrl Pts',(7.40504161293321,4.48843414683161,1.15928395680997));
#58528=CARTESIAN_POINT('Ctrl Pts',(7.46165237939758,4.45185198378456,1.32461816282306));
#58529=CARTESIAN_POINT('Ctrl Pts',(7.47510333060454,4.44874154321992,1.28004559878552));
#58530=CARTESIAN_POINT('Ctrl Pts',(7.4882729176626,4.44540260031461,1.23541025924608));
#58531=CARTESIAN_POINT('Ctrl Pts',(7.50115524253438,4.44182495202211,1.19071126177187));
#58532=CARTESIAN_POINT('',(7.49999999999943,4.44214493194956,1.19471687171392));
#58533=CARTESIAN_POINT('Ctrl Pts',(7.46165237939758,4.45185198378456,1.32461816282306));
#58534=CARTESIAN_POINT('Ctrl Pts',(7.47470152024064,4.44883445912125,1.28137708218025));
#58535=CARTESIAN_POINT('Ctrl Pts',(7.48748585582712,4.44560187997715,1.23807692051041));
#58536=CARTESIAN_POINT('Ctrl Pts',(7.50000000105064,4.44214493062788,1.19471687212266));
#58537=CARTESIAN_POINT('',(7.49999999999226,4.44238517355628,1.19033351972274));
#58538=CARTESIAN_POINT('Ctrl Pts',(7.50000000105118,4.44214493062774,1.19471687212079));
#58539=CARTESIAN_POINT('Ctrl Pts',(7.50000000037147,4.44222534202356,1.1932558707691));
#58540=CARTESIAN_POINT('Ctrl Pts',(7.49999999647456,4.4423054234084,1.19179476415888));
#58541=CARTESIAN_POINT('Ctrl Pts',(7.49999999999088,4.44238517355332,1.19033351972257));
#58542=CARTESIAN_POINT('Ctrl Pts',(7.49999999999083,4.44238517355338,1.19033351972196));
#58543=CARTESIAN_POINT('Ctrl Pts',(7.41273830259822,4.48255698032658,1.2010975229051));
#58544=CARTESIAN_POINT('Ctrl Pts',(7.32528335544063,4.52258076429358,1.21182190135916));
#58545=CARTESIAN_POINT('Ctrl Pts',(7.23748292043925,4.56288364865534,1.22262099986247));
#58546=CARTESIAN_POINT('Ctrl Pts',(7.21552165468913,4.57296449112441,1.22532214675415));
#58547=CARTESIAN_POINT('Ctrl Pts',(7.19439695636114,4.58266894946034,1.22792244418708));
#58548=CARTESIAN_POINT('Ctrl Pts',(7.17384635845268,4.59212072600811,1.23045504007998));
#58549=CARTESIAN_POINT('Ctrl Pts',(6.99737260418672,3.35466741224479,3.46502015180142));
#58550=CARTESIAN_POINT('Ctrl Pts',(6.872142618999,3.74844825878233,3.27785823931047));
#58551=CARTESIAN_POINT('Ctrl Pts',(6.69496761793157,4.16162987061384,3.08147524771389));
#58552=CARTESIAN_POINT('Ctrl Pts',(6.45213506509495,4.6201502592847,2.86354298002157));
#58553=CARTESIAN_POINT('Ctrl Pts',(7.15213252925707,3.3608045985668,3.37438271134571));
#58554=CARTESIAN_POINT('Ctrl Pts',(7.02199092199136,3.76260789239011,3.18165082839044));
#58555=CARTESIAN_POINT('Ctrl Pts',(6.83894619861566,4.18135148651518,2.98049590895782));
#58556=CARTESIAN_POINT('Ctrl Pts',(6.59045151405566,4.64358926304999,2.75873759472565));
#58557=CARTESIAN_POINT('Ctrl Pts',(7.30689245432741,3.3669417848888,3.28374527089));
#58558=CARTESIAN_POINT('Ctrl Pts',(7.17183922498373,3.77676752599789,3.08544341747041));
#58559=CARTESIAN_POINT('Ctrl Pts',(6.98292477929975,4.20107310241652,2.87951657020175));
#58560=CARTESIAN_POINT('Ctrl Pts',(6.72876796301638,4.66702826681527,2.65393220942972));
#58561=CARTESIAN_POINT('Ctrl Pts',(7.46165237939775,3.37307897121081,3.1931078304343));
#58562=CARTESIAN_POINT('Ctrl Pts',(7.32168752797609,3.79092715960566,2.98923600655038));
#58563=CARTESIAN_POINT('Ctrl Pts',(7.12690335998383,4.22079471831786,2.77853723144567));
#58564=CARTESIAN_POINT('Ctrl Pts',(6.86708441197709,4.69046727058056,2.54912682413379));
#58565=CARTESIAN_POINT('Ctrl Pts',(6.49649612061064,4.53548229371214,2.9037852073991));
#58566=CARTESIAN_POINT('Ctrl Pts',(6.70189613387518,4.13912090191365,3.09217363913432));
#58567=CARTESIAN_POINT('Ctrl Pts',(6.85768162696566,3.77623926085462,3.26464932591708));
#58568=CARTESIAN_POINT('Ctrl Pts',(6.97303770582829,3.42946324032328,3.42947009812916));
#58569=CARTESIAN_POINT('',(7.46165237939775,3.37307897121081,3.1931078304343));
#58570=CARTESIAN_POINT('Ctrl Pts',(7.46165237939775,3.37307897121081,3.1931078304343));
#58571=CARTESIAN_POINT('Ctrl Pts',(7.36571703908279,3.36927454278329,3.24929378226545));
#58572=CARTESIAN_POINT('Ctrl Pts',(7.26978169876783,3.36547011435578,3.3054797340966));
#58573=CARTESIAN_POINT('Ctrl Pts',(7.17384635845287,3.36166568592826,3.36166568592776));
#58574=CARTESIAN_POINT('Ctrl Pts',(7.46165237939775,3.37307897121081,3.1931078304343));
#58575=CARTESIAN_POINT('Ctrl Pts',(7.33663088231331,3.74631557694812,3.01100239198735));
#58576=CARTESIAN_POINT('Ctrl Pts',(7.16787076968672,4.12914206176923,2.82344994300742));
#58577=CARTESIAN_POINT('Ctrl Pts',(6.94809164225641,4.54136079998446,2.62198045928535));
#58578=CARTESIAN_POINT('Ctrl Pts',(7.17384635845274,3.36166568592805,3.36166568592792));
#58579=CARTESIAN_POINT('Ctrl Pts',(7.18694338462388,3.38104574649207,3.32129593728098));
#58580=CARTESIAN_POINT('Ctrl Pts',(7.1999334636689,3.40036251963242,3.28086209719208));
#58581=CARTESIAN_POINT('Ctrl Pts',(7.21281435373094,3.41961281443653,3.2403619360835));
#58582=CARTESIAN_POINT('Ctrl Pts',(7.26978169876769,3.30547973409671,3.36547011435572));
#58583=CARTESIAN_POINT('Ctrl Pts',(7.28299669995076,3.324930628297,3.32517155090754));
#58584=CARTESIAN_POINT('Ctrl Pts',(7.29604661500013,3.34428383052122,3.28477405438149));
#58585=CARTESIAN_POINT('Ctrl Pts',(7.30892798333209,3.36353441520062,3.24427418314824));
#58586=CARTESIAN_POINT('Ctrl Pts',(7.36571703908264,3.24929378226538,3.36927454278352));
#58587=CARTESIAN_POINT('Ctrl Pts',(7.37905001527765,3.26881551010194,3.32904716453411));
#58588=CARTESIAN_POINT('Ctrl Pts',(7.39215976633137,3.28820514141002,3.28868601157091));
#58589=CARTESIAN_POINT('Ctrl Pts',(7.40504161293323,3.30745601596472,3.24818643021297));
#58590=CARTESIAN_POINT('Ctrl Pts',(7.46165237939758,3.19310783043405,3.37307897121132));
#58591=CARTESIAN_POINT('Ctrl Pts',(7.47510333060454,3.21270039190688,3.33292277816068));
#58592=CARTESIAN_POINT('Ctrl Pts',(7.4882729176626,3.23212645229882,3.29259796876032));
#58593=CARTESIAN_POINT('Ctrl Pts',(7.50115524253438,3.25137761672882,3.25209867727771));
#58594=CARTESIAN_POINT('',(7.49999999999943,3.24965192250365,3.25572762720891));
#58595=CARTESIAN_POINT('Ctrl Pts',(7.46165237939758,3.19310783043405,3.37307897121132));
#58596=CARTESIAN_POINT('Ctrl Pts',(7.47470152024065,3.21211511774048,3.3341223345559));
#58597=CARTESIAN_POINT('Ctrl Pts',(7.48748585582712,3.23096570291687,3.2950070049898));
#58598=CARTESIAN_POINT('Ctrl Pts',(7.50000000105064,3.24965192115468,3.25572762690205));
#58599=CARTESIAN_POINT('',(7.49999999999234,3.25205165383366,3.25205165383413));
#58600=CARTESIAN_POINT('Ctrl Pts',(7.50000000105118,3.24965192115549,3.25572762690036));
#58601=CARTESIAN_POINT('Ctrl Pts',(7.50000000037148,3.25045206029546,3.25450256807911));
#58602=CARTESIAN_POINT('Ctrl Pts',(7.49999999647522,3.25125196611448,3.25327725332823));
#58603=CARTESIAN_POINT('Ctrl Pts',(7.49999999999097,3.25205165383121,3.25205165383252));
#58604=CARTESIAN_POINT('Ctrl Pts',(7.49999999999092,3.25205165383156,3.25205165383202));
#58605=CARTESIAN_POINT('Ctrl Pts',(7.41251809600285,3.28153366858747,3.28153366858761));
#58606=CARTESIAN_POINT('Ctrl Pts',(7.32483941486394,3.31090761336157,3.3109076646946));
#58607=CARTESIAN_POINT('Ctrl Pts',(7.23681685935962,3.34048647397502,3.34048648878989));
#58608=CARTESIAN_POINT('Ctrl Pts',(7.21511249441227,3.34777994985518,3.3477799556655));
#58609=CARTESIAN_POINT('Ctrl Pts',(7.19420493717939,3.35481115621011,3.35481115621012));
#58610=CARTESIAN_POINT('Ctrl Pts',(7.17384635845274,3.36166568592805,3.36166568592792));
#58611=CARTESIAN_POINT('Ctrl Pts',(6.99737260418672,1.17271712435108,4.67812918220743));
#58612=CARTESIAN_POINT('Ctrl Pts',(6.872142618999,1.60732229722181,4.71293263463817));
#58613=CARTESIAN_POINT('Ctrl Pts',(6.69496761793157,2.06333956524279,4.7494507809601));
#58614=CARTESIAN_POINT('Ctrl Pts',(6.45213506509495,2.56939600383103,4.78997609516963));
#58615=CARTESIAN_POINT('Ctrl Pts',(7.15213252925707,1.22335080384155,4.6027034493998));
#58616=CARTESIAN_POINT('Ctrl Pts',(7.02199092199136,1.66768860509444,4.63669438955298));
#58617=CARTESIAN_POINT('Ctrl Pts',(6.83894619861566,2.13090865499507,4.67186091629066));
#58618=CARTESIAN_POINT('Ctrl Pts',(6.59045151405566,2.64209746917913,4.71093147093258));
#58619=CARTESIAN_POINT('Ctrl Pts',(7.30689245432741,1.27398448333202,4.52727771659216));
#58620=CARTESIAN_POINT('Ctrl Pts',(7.17183922498372,1.72805491296707,4.56045614446779));
#58621=CARTESIAN_POINT('Ctrl Pts',(6.98292477929974,2.19847774474734,4.59427105162121));
#58622=CARTESIAN_POINT('Ctrl Pts',(6.72876796301637,2.71479893452723,4.63188684669553));
#58623=CARTESIAN_POINT('Ctrl Pts',(7.46165237939775,1.32461816282249,4.45185198378452));
#58624=CARTESIAN_POINT('Ctrl Pts',(7.32168752797609,1.7884212208397,4.48421789938261));
#58625=CARTESIAN_POINT('Ctrl Pts',(7.12690335998383,2.26604683449962,4.51668118695177));
#58626=CARTESIAN_POINT('Ctrl Pts',(6.86708441197709,2.78750039987533,4.55284222245849));
#58627=CARTESIAN_POINT('Ctrl Pts',(6.49649612061063,2.47595028106968,4.78249290359715));
#58628=CARTESIAN_POINT('Ctrl Pts',(6.70189613387517,2.03849703082522,4.74746137535973));
#58629=CARTESIAN_POINT('Ctrl Pts',(6.85768162696566,1.63799446770973,4.71538888111925));
#58630=CARTESIAN_POINT('Ctrl Pts',(6.97303770582829,1.25526723840028,4.68473984666061));
#58631=CARTESIAN_POINT('',(7.46165237939775,1.32461816282249,4.45185198378452));
#58632=CARTESIAN_POINT('Ctrl Pts',(7.46165237939775,1.32461816282249,4.45185198378452));
#58633=CARTESIAN_POINT('Ctrl Pts',(7.36571703908279,1.29323045524181,4.49860823119235));
#58634=CARTESIAN_POINT('Ctrl Pts',(7.26978169876783,1.26184274766112,4.54536447860018));
#58635=CARTESIAN_POINT('Ctrl Pts',(7.17384635845286,1.23045504008043,4.59212072600801));
#58636=CARTESIAN_POINT('Ctrl Pts',(7.46165237939775,1.32461816282249,4.45185198378452));
#58637=CARTESIAN_POINT('Ctrl Pts',(7.33663088231331,1.73890326423675,4.48076235079082));
#58638=CARTESIAN_POINT('Ctrl Pts',(7.16787076968672,2.1642169498233,4.50975040784277));
#58639=CARTESIAN_POINT('Ctrl Pts',(6.94809164225641,2.62194359089469,4.54138208595974));
#58640=CARTESIAN_POINT('Ctrl Pts',(7.17384635845275,1.23045504008017,4.59212072600804));
#58641=CARTESIAN_POINT('Ctrl Pts',(7.18694338462388,1.26742353917896,4.56684952841741));
#58642=CARTESIAN_POINT('Ctrl Pts',(7.1999334636689,1.3043692754821,4.54149118229804));
#58643=CARTESIAN_POINT('Ctrl Pts',(7.21281435373095,1.34129060036708,4.5160421613227));
#58644=CARTESIAN_POINT('Ctrl Pts',(7.26978169876769,1.17989436424452,4.56732248175773));
#58645=CARTESIAN_POINT('Ctrl Pts',(7.28299669995077,1.21688861447239,4.54214834917574));
#58646=CARTESIAN_POINT('Ctrl Pts',(7.29604661500014,1.25384772750616,4.51683969204699));
#58647=CARTESIAN_POINT('Ctrl Pts',(7.30892798333209,1.29076915849286,4.49139106704869));
#58648=CARTESIAN_POINT('Ctrl Pts',(7.36571703908264,1.12933368840888,4.54252423750742));
#58649=CARTESIAN_POINT('Ctrl Pts',(7.37905001527765,1.16635368976581,4.51744716993406));
#58650=CARTESIAN_POINT('Ctrl Pts',(7.39215976633137,1.20332617953023,4.49218820179594));
#58651=CARTESIAN_POINT('Ctrl Pts',(7.40504161293324,1.24024771661863,4.46673997277468));
#58652=CARTESIAN_POINT('Ctrl Pts',(7.46165237939758,1.07877301257324,4.51772599325711));
#58653=CARTESIAN_POINT('Ctrl Pts',(7.47510333060454,1.11581876505924,4.49274599069239));
#58654=CARTESIAN_POINT('Ctrl Pts',(7.4882729176626,1.15280463155429,4.46753671154489));
#58655=CARTESIAN_POINT('Ctrl Pts',(7.50115524253438,1.18972627474441,4.44208887850067));
#58656=CARTESIAN_POINT('',(7.49999999999234,1.19033351972209,4.44238517355638));
#58657=CARTESIAN_POINT('Ctrl Pts',(7.50000000105118,1.18641730372738,4.44436879327628));
#58658=CARTESIAN_POINT('Ctrl Pts',(7.50000000037148,1.18772277427295,4.4437079306274));
#58659=CARTESIAN_POINT('Ctrl Pts',(7.49999999647595,1.18902817040918,4.44304672983401));
#58660=CARTESIAN_POINT('Ctrl Pts',(7.49999999999097,1.19033351972076,4.44238517355376));
#58661=CARTESIAN_POINT('Ctrl Pts',(7.49999999999092,1.19033351972131,4.44238517355351));
#58662=CARTESIAN_POINT('Ctrl Pts',(7.4125189586941,1.20112457966122,4.4826579575159));
#58663=CARTESIAN_POINT('Ctrl Pts',(7.32484115407291,1.21187605713238,4.52278315794289));
#58664=CARTESIAN_POINT('Ctrl Pts',(7.23681946879609,1.22270258210925,4.56318819945531));
#58665=CARTESIAN_POINT('Ctrl Pts',(7.21511409889809,1.22537230751378,4.5731517257047));
#58666=CARTESIAN_POINT('Ctrl Pts',(7.19420569065439,1.22794601521628,4.58275691773891));
#58667=CARTESIAN_POINT('Ctrl Pts',(7.17384635845275,1.23045504008016,4.59212072600804));
#58668=CARTESIAN_POINT('Ctrl Pts',(6.97302668913468,-1.25527236874723,4.68474025750198));
#58669=CARTESIAN_POINT('Ctrl Pts',(6.84940428632249,-0.916731434795263,
4.91809665777761));
#58670=CARTESIAN_POINT('Ctrl Pts',(6.67964184929033,-0.561440197692398,
5.16299904867006));
#58671=CARTESIAN_POINT('Ctrl Pts',(6.45213506520422,-0.169825836073017,
5.43293898372295));
#58672=CARTESIAN_POINT('Ctrl Pts',(7.12684466416248,-1.17205861623371,4.64550450560439));
#58673=CARTESIAN_POINT('Ctrl Pts',(6.99850389456238,-0.825458101169696,
4.8825619686287));
#58674=CARTESIAN_POINT('Ctrl Pts',(6.82326307870631,-0.463802289985809,
5.12967124535383));
#58675=CARTESIAN_POINT('Ctrl Pts',(6.59045151416748,-0.0673422080730113,
5.40083506377453));
#58676=CARTESIAN_POINT('Ctrl Pts',(7.28066263919028,-1.0888448637202,4.6062687537068));
#58677=CARTESIAN_POINT('Ctrl Pts',(7.14760350280226,-0.73418476754413,4.8470272794798));
#58678=CARTESIAN_POINT('Ctrl Pts',(6.9668843081223,-0.366164382279219,5.09634344203759));
#58679=CARTESIAN_POINT('Ctrl Pts',(6.72876796313074,0.0351414199269946,
5.36873114382612));
#58680=CARTESIAN_POINT('Ctrl Pts',(7.43448061421808,-1.00563111120669,4.56703300180921));
#58681=CARTESIAN_POINT('Ctrl Pts',(7.29670311104215,-0.642911433918564,
4.81149259033089));
#58682=CARTESIAN_POINT('Ctrl Pts',(7.11050553753828,-0.26852647457263,5.06301563872136));
#58683=CARTESIAN_POINT('Ctrl Pts',(6.867084412094,0.137625047927001,5.3366272238777));
#58684=CARTESIAN_POINT('Ctrl Pts',(6.49649473556578,-0.247010070495211,
5.37973586027038));
#58685=CARTESIAN_POINT('Ctrl Pts',(6.70188214815405,-0.608335026879687,
5.13067442427992));
#58686=CARTESIAN_POINT('Ctrl Pts',(6.85757546768223,-0.939108279979382,
4.90267228950186));
#58687=CARTESIAN_POINT('Ctrl Pts',(6.97302668913468,-1.25527236874723,4.68474025750198));
#58688=CARTESIAN_POINT('Ctrl Pts',(7.2128143537305,1.09642934688643,4.5816525364507));
#58689=CARTESIAN_POINT('Ctrl Pts',(7.19993346366857,1.14112866266591,4.58523137267427));
#58690=CARTESIAN_POINT('Ctrl Pts',(7.18694338462366,1.18580378192567,4.58871947646));
#58691=CARTESIAN_POINT('Ctrl Pts',(7.17384635845263,1.23045504008035,4.59212072600812));
#58692=CARTESIAN_POINT('Ctrl Pts',(7.30892798333179,1.12785665184803,4.53504334164122));
#58693=CARTESIAN_POINT('Ctrl Pts',(7.29604661499993,1.17255586152576,4.53862178188775));
#58694=CARTESIAN_POINT('Ctrl Pts',(7.28299669995066,1.21721772087875,4.54206016537998));
#58695=CARTESIAN_POINT('Ctrl Pts',(7.26978169876767,1.26184274766107,4.54536447860025));
#58696=CARTESIAN_POINT('Ctrl Pts',(7.40504161293309,1.15928395680962,4.48843414683175));
#58697=CARTESIAN_POINT('Ctrl Pts',(7.3921597663313,1.20398306038561,4.49201219110123));
#58698=CARTESIAN_POINT('Ctrl Pts',(7.37905001527766,1.24863165983184,4.49540085429997));
#58699=CARTESIAN_POINT('Ctrl Pts',(7.36571703908271,1.29323045524178,4.49860823119239));
#58700=CARTESIAN_POINT('Ctrl Pts',(7.50115524253438,1.19071126177122,4.44182495202228));
#58701=CARTESIAN_POINT('Ctrl Pts',(7.48827291766266,1.23541025924546,4.44540260031471));
#58702=CARTESIAN_POINT('Ctrl Pts',(7.47510333060465,1.28004559878492,4.44874154321995));
#58703=CARTESIAN_POINT('Ctrl Pts',(7.46165237939775,1.32461816282249,4.45185198378452));
#58704=CARTESIAN_POINT('',(7.49999999999943,1.19471687171331,4.44214493194972));
#58705=CARTESIAN_POINT('Ctrl Pts',(7.49999999999097,1.19033351972193,4.44238517355345));
#58706=CARTESIAN_POINT('Ctrl Pts',(7.49999999569756,1.19179469976444,4.44230542728599));
#58707=CARTESIAN_POINT('Ctrl Pts',(7.50000000037144,1.1932558035927,4.44222534572098));
#58708=CARTESIAN_POINT('Ctrl Pts',(7.50000000105118,1.19471687212018,4.4421449306279));
#58709=CARTESIAN_POINT('Ctrl Pts',(7.50000000105064,1.19471687212205,4.44214493062805));
#58710=CARTESIAN_POINT('Ctrl Pts',(7.48748585582718,1.23807692050981,4.44560187997725));
#58711=CARTESIAN_POINT('Ctrl Pts',(7.47470152024076,1.28137708217967,4.44883445912128));
#58712=CARTESIAN_POINT('Ctrl Pts',(7.46165237939775,1.32461816282249,4.45185198378452));
#58713=CARTESIAN_POINT('Ctrl Pts',(7.21281435373049,3.24036193608378,3.4196128144365));
#58714=CARTESIAN_POINT('Ctrl Pts',(7.19993346366856,3.28086209719237,3.40036251963235));
#58715=CARTESIAN_POINT('Ctrl Pts',(7.18694338462365,3.32129593728129,3.38104574649196));
#58716=CARTESIAN_POINT('Ctrl Pts',(7.17384635845263,3.36166568592825,3.3616656859279));
#58717=CARTESIAN_POINT('Ctrl Pts',(7.30892798333179,3.24427418314827,3.36353441520076));
#58718=CARTESIAN_POINT('Ctrl Pts',(7.29604661499993,3.28477405438153,3.34428383052131));
#58719=CARTESIAN_POINT('Ctrl Pts',(7.28299669995065,3.32517155090759,3.32493062829704));
#58720=CARTESIAN_POINT('Ctrl Pts',(7.26978169876767,3.36547011435577,3.3054797340967));
#58721=CARTESIAN_POINT('Ctrl Pts',(7.40504161293308,3.24818643021275,3.30745601596502));
#58722=CARTESIAN_POINT('Ctrl Pts',(7.39215976633129,3.28868601157069,3.28820514141026));
#58723=CARTESIAN_POINT('Ctrl Pts',(7.37905001527765,3.32904716453388,3.26881551010212));
#58724=CARTESIAN_POINT('Ctrl Pts',(7.36571703908271,3.36927454278329,3.2492937822655));
#58725=CARTESIAN_POINT('Ctrl Pts',(7.50115524253438,3.25209867727724,3.25137761672928));
#58726=CARTESIAN_POINT('Ctrl Pts',(7.48827291766266,3.29259796875984,3.23212645229921));
#58727=CARTESIAN_POINT('Ctrl Pts',(7.47510333060465,3.33292277816018,3.2127003919072));
#58728=CARTESIAN_POINT('Ctrl Pts',(7.46165237939775,3.37307897121081,3.1931078304343));
#58729=CARTESIAN_POINT('',(7.49999999999943,3.25572762720846,3.24965192250411));
#58730=CARTESIAN_POINT('Ctrl Pts',(7.49999999999097,3.25205165383206,3.25205165383167));
#58731=CARTESIAN_POINT('Ctrl Pts',(7.49999999570083,3.25327719982305,3.25125200145742));
#58732=CARTESIAN_POINT('Ctrl Pts',(7.50000000037144,3.25450251208352,3.25045209686877));
#58733=CARTESIAN_POINT('Ctrl Pts',(7.50000000105118,3.25572762689991,3.24965192115593));
#58734=CARTESIAN_POINT('Ctrl Pts',(7.50000000105064,3.2557276269016,3.24965192115513));
#58735=CARTESIAN_POINT('Ctrl Pts',(7.48748585582718,3.29500700498933,3.23096570291725));
#58736=CARTESIAN_POINT('Ctrl Pts',(7.47470152024076,3.33412233455541,3.21211511774079));
#58737=CARTESIAN_POINT('Ctrl Pts',(7.46165237939775,3.37307897121081,3.1931078304343));
#58738=CARTESIAN_POINT('Ctrl Pts',(7.21281435373043,4.51604216132295,1.34129060036694));
#58739=CARTESIAN_POINT('Ctrl Pts',(7.1999334636685,4.54149118229828,1.30436927548192));
#58740=CARTESIAN_POINT('Ctrl Pts',(7.18694338462359,4.56684952841764,1.26742353917874));
#58741=CARTESIAN_POINT('Ctrl Pts',(7.17384635845257,4.59212072600827,1.23045504007991));
#58742=CARTESIAN_POINT('Ctrl Pts',(7.30892798333175,4.4913910670488,1.29076915849297));
#58743=CARTESIAN_POINT('Ctrl Pts',(7.29604661499989,4.51683969204708,1.25384772750623));
#58744=CARTESIAN_POINT('Ctrl Pts',(7.28299669995061,4.5421483491758,1.21688861447241));
#58745=CARTESIAN_POINT('Ctrl Pts',(7.26978169876763,4.56732248175777,1.17989436424451));
#58746=CARTESIAN_POINT('Ctrl Pts',(7.40504161293306,4.46673997277466,1.240247716619));
#58747=CARTESIAN_POINT('Ctrl Pts',(7.39215976633127,4.49218820179588,1.20332617953055));
#58748=CARTESIAN_POINT('Ctrl Pts',(7.37905001527763,4.51744716993396,1.16635368976609));
#58749=CARTESIAN_POINT('Ctrl Pts',(7.36571703908269,4.54252423750728,1.12933368840911));
#58750=CARTESIAN_POINT('Ctrl Pts',(7.50115524253438,4.44208887850051,1.18972627474503));
#58751=CARTESIAN_POINT('Ctrl Pts',(7.48827291766266,4.46753671154468,1.15280463155486));
#58752=CARTESIAN_POINT('Ctrl Pts',(7.47510333060465,4.49274599069213,1.11581876505976));
#58753=CARTESIAN_POINT('Ctrl Pts',(7.46165237939775,4.51772599325679,1.07877301257371));
#58754=CARTESIAN_POINT('',(7.49999999999943,4.44436879421741,1.18641730474127));
#58755=CARTESIAN_POINT('Ctrl Pts',(7.49999999999088,4.44238517355364,1.1903335197214));
#58756=CARTESIAN_POINT('Ctrl Pts',(7.49999999570487,4.44304670138692,1.18902822733552));
#58757=CARTESIAN_POINT('Ctrl Pts',(7.50000000037144,4.4437079006456,1.1877228334994));
#58758=CARTESIAN_POINT('Ctrl Pts',(7.50000000105118,4.44436879327611,1.18641730372799));
#58759=CARTESIAN_POINT('Ctrl Pts',(7.50000000105064,4.44436879327717,1.18641730372645));
#58760=CARTESIAN_POINT('Ctrl Pts',(7.48748585582718,4.46904262342706,1.15059487498792));
#58761=CARTESIAN_POINT('Ctrl Pts',(7.47470152024076,4.49349219992046,1.11471212456586));
#58762=CARTESIAN_POINT('Ctrl Pts',(7.46165237939775,4.51772599325679,1.07877301257371));
#58763=CARTESIAN_POINT('Ctrl Pts',(7.2128143537299,-4.51604216132309,-1.34129060036722));
#58764=CARTESIAN_POINT('Ctrl Pts',(7.19993346366797,-4.54149118229842,-1.3043692754822));
#58765=CARTESIAN_POINT('Ctrl Pts',(7.18694338462306,-4.56684952841778,-1.26742353917902));
#58766=CARTESIAN_POINT('Ctrl Pts',(7.17384635845204,-4.5921207260084,-1.23045504008019));
#58767=CARTESIAN_POINT('Ctrl Pts',(7.30892798333139,-4.49139106704889,-1.29076915849316));
#58768=CARTESIAN_POINT('Ctrl Pts',(7.29604661499953,-4.51683969204717,-1.25384772750642));
#58769=CARTESIAN_POINT('Ctrl Pts',(7.28299669995026,-4.54214834917589,-1.2168886144726));
#58770=CARTESIAN_POINT('Ctrl Pts',(7.26978169876728,-4.56732248175787,-1.17989436424469));
#58771=CARTESIAN_POINT('Ctrl Pts',(7.40504161293288,-4.4667399727747,-1.24024771661909));
#58772=CARTESIAN_POINT('Ctrl Pts',(7.39215976633109,-4.49218820179592,-1.20332617953064));
#58773=CARTESIAN_POINT('Ctrl Pts',(7.37905001527746,-4.51744716993401,-1.16635368976618));
#58774=CARTESIAN_POINT('Ctrl Pts',(7.36571703908252,-4.54252423750733,-1.1293336884092));
#58775=CARTESIAN_POINT('Ctrl Pts',(7.50115524253438,-4.44208887850051,-1.18972627474503));
#58776=CARTESIAN_POINT('Ctrl Pts',(7.48827291766266,-4.46753671154468,-1.15280463155487));
#58777=CARTESIAN_POINT('Ctrl Pts',(7.47510333060465,-4.49274599069213,-1.11581876505976));
#58778=CARTESIAN_POINT('Ctrl Pts',(7.46165237939775,-4.51772599325679,-1.07877301257371));
#58779=CARTESIAN_POINT('Ctrl Pts',(7.49999999999088,-4.44238517355363,-1.1903335197214));
#58780=CARTESIAN_POINT('Ctrl Pts',(7.49999999570487,-4.44304670138692,-1.18902822733552));
#58781=CARTESIAN_POINT('Ctrl Pts',(7.50000000037144,-4.4437079006456,-1.1877228334994));
#58782=CARTESIAN_POINT('Ctrl Pts',(7.50000000105118,-4.44436879327611,-1.18641730372799));
#58783=CARTESIAN_POINT('Ctrl Pts',(7.2128143537299,-3.24036193608375,-3.41961281443685));
#58784=CARTESIAN_POINT('Ctrl Pts',(7.19993346366797,-3.28086209719235,-3.4003625196327));
#58785=CARTESIAN_POINT('Ctrl Pts',(7.18694338462306,-3.32129593728126,-3.38104574649231));
#58786=CARTESIAN_POINT('Ctrl Pts',(7.17384635845203,-3.36166568592822,-3.36166568592825));
#58787=CARTESIAN_POINT('Ctrl Pts',(7.30892798333139,-3.24427418314825,-3.36353441520099));
#58788=CARTESIAN_POINT('Ctrl Pts',(7.29604661499953,-3.28477405438151,-3.34428383052154));
#58789=CARTESIAN_POINT('Ctrl Pts',(7.28299669995025,-3.32517155090757,-3.32493062829727));
#58790=CARTESIAN_POINT('Ctrl Pts',(7.26978169876727,-3.36547011435575,-3.30547973409693));
#58791=CARTESIAN_POINT('Ctrl Pts',(7.40504161293289,-3.24818643021274,-3.30745601596514));
#58792=CARTESIAN_POINT('Ctrl Pts',(7.3921597663311,-3.28868601157068,-3.28820514141038));
#58793=CARTESIAN_POINT('Ctrl Pts',(7.37905001527746,-3.32904716453387,-3.26881551010224));
#58794=CARTESIAN_POINT('Ctrl Pts',(7.36571703908251,-3.36927454278328,-3.24929378226561));
#58795=CARTESIAN_POINT('Ctrl Pts',(7.50115524253438,-3.25209867727724,-3.25137761672928));
#58796=CARTESIAN_POINT('Ctrl Pts',(7.48827291766266,-3.29259796875984,-3.23212645229922));
#58797=CARTESIAN_POINT('Ctrl Pts',(7.47510333060465,-3.33292277816018,-3.2127003919072));
#58798=CARTESIAN_POINT('Ctrl Pts',(7.46165237939775,-3.37307897121081,-3.1931078304343));
#58799=CARTESIAN_POINT('',(7.49999999999943,-3.25572762720846,-3.2496519225041));
#58800=CARTESIAN_POINT('Ctrl Pts',(7.49999999999097,-3.25205165383206,-3.25205165383167));
#58801=CARTESIAN_POINT('Ctrl Pts',(7.49999999570083,-3.25327719982305,-3.25125200145742));
#58802=CARTESIAN_POINT('Ctrl Pts',(7.50000000037144,-3.25450251208352,-3.25045209686877));
#58803=CARTESIAN_POINT('Ctrl Pts',(7.50000000105118,-3.25572762689991,-3.24965192115593));
#58804=CARTESIAN_POINT('Ctrl Pts',(7.50000000105064,-3.2557276269016,-3.24965192115513));
#58805=CARTESIAN_POINT('Ctrl Pts',(7.48748585582718,-3.29500700498933,-3.23096570291725));
#58806=CARTESIAN_POINT('Ctrl Pts',(7.47470152024076,-3.33412233455541,-3.21211511774079));
#58807=CARTESIAN_POINT('Ctrl Pts',(7.46165237939775,-3.37307897121081,-3.1931078304343));
#58808=CARTESIAN_POINT('Ctrl Pts',(7.21281435372989,-1.09642934688624,-4.58165253645099));
#58809=CARTESIAN_POINT('Ctrl Pts',(7.19993346366796,-1.14112866266571,-4.58523137267456));
#58810=CARTESIAN_POINT('Ctrl Pts',(7.18694338462305,-1.18580378192547,-4.5887194764603));
#58811=CARTESIAN_POINT('Ctrl Pts',(7.17384635845202,-1.23045504008016,-4.59212072600842));
#58812=CARTESIAN_POINT('Ctrl Pts',(7.30892798333139,-1.1278566518479,-4.53504334164142));
#58813=CARTESIAN_POINT('Ctrl Pts',(7.29604661499952,-1.17255586152563,-4.53862178188795));
#58814=CARTESIAN_POINT('Ctrl Pts',(7.28299669995025,-1.21721772087862,-4.54206016538018));
#58815=CARTESIAN_POINT('Ctrl Pts',(7.26978169876727,-1.26184274766094,-4.54536447860045));
#58816=CARTESIAN_POINT('Ctrl Pts',(7.40504161293288,-1.15928395680956,-4.48843414683185));
#58817=CARTESIAN_POINT('Ctrl Pts',(7.39215976633109,-1.20398306038554,-4.49201219110133));
#58818=CARTESIAN_POINT('Ctrl Pts',(7.37905001527745,-1.24863165983177,-4.49540085430006));
#58819=CARTESIAN_POINT('Ctrl Pts',(7.36571703908251,-1.29323045524171,-4.49860823119249));
#58820=CARTESIAN_POINT('Ctrl Pts',(7.50115524253438,-1.19071126177122,-4.44182495202228));
#58821=CARTESIAN_POINT('Ctrl Pts',(7.48827291766266,-1.23541025924546,-4.44540260031471));
#58822=CARTESIAN_POINT('Ctrl Pts',(7.47510333060465,-1.28004559878492,-4.44874154321995));
#58823=CARTESIAN_POINT('Ctrl Pts',(7.46165237939775,-1.32461816282249,-4.45185198378452));
#58824=CARTESIAN_POINT('',(7.49999999999943,-1.1947168717133,-4.44214493194972));
#58825=CARTESIAN_POINT('Ctrl Pts',(7.49999999999097,-1.19033351972193,-4.44238517355345));
#58826=CARTESIAN_POINT('Ctrl Pts',(7.49999999569755,-1.19179469976444,-4.44230542728599));
#58827=CARTESIAN_POINT('Ctrl Pts',(7.50000000037144,-1.1932558035927,-4.44222534572098));
#58828=CARTESIAN_POINT('Ctrl Pts',(7.50000000105118,-1.19471687212018,-4.4421449306279));
#58829=CARTESIAN_POINT('Ctrl Pts',(7.50000000105064,-1.19471687212205,-4.44214493062805));
#58830=CARTESIAN_POINT('Ctrl Pts',(7.48748585582718,-1.23807692050981,-4.44560187997725));
#58831=CARTESIAN_POINT('Ctrl Pts',(7.47470152024076,-1.28137708217967,-4.44883445912128));
#58832=CARTESIAN_POINT('Ctrl Pts',(7.46165237939775,-1.32461816282249,-4.45185198378452));
#58833=CARTESIAN_POINT('Ctrl Pts',(7.21281435372989,1.34129060036722,-4.51604216132309));
#58834=CARTESIAN_POINT('Ctrl Pts',(7.19993346366796,1.3043692754822,-4.54149118229842));
#58835=CARTESIAN_POINT('Ctrl Pts',(7.18694338462305,1.26742353917902,-4.56684952841778));
#58836=CARTESIAN_POINT('Ctrl Pts',(7.17384635845203,1.23045504008019,-4.59212072600841));
#58837=CARTESIAN_POINT('Ctrl Pts',(7.30892798333139,1.29076915849316,-4.4913910670489));
#58838=CARTESIAN_POINT('Ctrl Pts',(7.29604661499953,1.25384772750642,-4.51683969204717));
#58839=CARTESIAN_POINT('Ctrl Pts',(7.28299669995025,1.2168886144726,-4.5421483491759));
#58840=CARTESIAN_POINT('Ctrl Pts',(7.26978169876727,1.17989436424469,-4.56732248175787));
#58841=CARTESIAN_POINT('Ctrl Pts',(7.40504161293288,1.24024771661909,-4.4667399727747));
#58842=CARTESIAN_POINT('Ctrl Pts',(7.39215976633109,1.20332617953064,-4.49218820179592));
#58843=CARTESIAN_POINT('Ctrl Pts',(7.37905001527745,1.16635368976618,-4.51744716993401));
#58844=CARTESIAN_POINT('Ctrl Pts',(7.36571703908251,1.1293336884092,-4.54252423750733));
#58845=CARTESIAN_POINT('Ctrl Pts',(7.50115524253438,1.18972627474503,-4.44208887850051));
#58846=CARTESIAN_POINT('Ctrl Pts',(7.48827291766266,1.15280463155486,-4.46753671154468));
#58847=CARTESIAN_POINT('Ctrl Pts',(7.47510333060465,1.11581876505976,-4.49274599069213));
#58848=CARTESIAN_POINT('Ctrl Pts',(7.46165237939775,1.07877301257371,-4.51772599325679));
#58849=CARTESIAN_POINT('',(7.49999999999943,1.18641730474126,-4.44436879421741));
#58850=CARTESIAN_POINT('Ctrl Pts',(7.49999999999088,1.19033351972139,-4.44238517355364));
#58851=CARTESIAN_POINT('Ctrl Pts',(7.49999999570486,1.18902822733552,-4.44304670138692));
#58852=CARTESIAN_POINT('Ctrl Pts',(7.50000000037144,1.1877228334994,-4.4437079006456));
#58853=CARTESIAN_POINT('Ctrl Pts',(7.50000000105118,1.18641730372799,-4.44436879327611));
#58854=CARTESIAN_POINT('Ctrl Pts',(7.50000000105064,1.18641730372645,-4.44436879327718));
#58855=CARTESIAN_POINT('Ctrl Pts',(7.48748585582718,1.15059487498792,-4.46904262342707));
#58856=CARTESIAN_POINT('Ctrl Pts',(7.47470152024076,1.11471212456586,-4.49349219992046));
#58857=CARTESIAN_POINT('Ctrl Pts',(7.46165237939775,1.07877301257371,-4.51772599325679));
#58858=CARTESIAN_POINT('Ctrl Pts',(7.21281435372989,3.41961281443685,-3.24036193608376));
#58859=CARTESIAN_POINT('Ctrl Pts',(7.19993346366796,3.4003625196327,-3.28086209719235));
#58860=CARTESIAN_POINT('Ctrl Pts',(7.18694338462305,3.38104574649231,-3.32129593728127));
#58861=CARTESIAN_POINT('Ctrl Pts',(7.17384635845203,3.36166568592825,-3.36166568592822));
#58862=CARTESIAN_POINT('Ctrl Pts',(7.30892798333139,3.36353441520099,-3.24427418314825));
#58863=CARTESIAN_POINT('Ctrl Pts',(7.29604661499953,3.34428383052154,-3.28477405438151));
#58864=CARTESIAN_POINT('Ctrl Pts',(7.28299669995025,3.32493062829727,-3.32517155090757));
#58865=CARTESIAN_POINT('Ctrl Pts',(7.26978169876727,3.30547973409693,-3.36547011435575));
#58866=CARTESIAN_POINT('Ctrl Pts',(7.40504161293288,3.30745601596514,-3.24818643021275));
#58867=CARTESIAN_POINT('Ctrl Pts',(7.39215976633109,3.28820514141038,-3.28868601157068));
#58868=CARTESIAN_POINT('Ctrl Pts',(7.37905001527745,3.26881551010224,-3.32904716453388));
#58869=CARTESIAN_POINT('Ctrl Pts',(7.36571703908251,3.24929378226561,-3.36927454278328));
#58870=CARTESIAN_POINT('Ctrl Pts',(7.50115524253438,3.25137761672928,-3.25209867727724));
#58871=CARTESIAN_POINT('Ctrl Pts',(7.48827291766266,3.23212645229921,-3.29259796875984));
#58872=CARTESIAN_POINT('Ctrl Pts',(7.47510333060465,3.2127003919072,-3.33292277816018));
#58873=CARTESIAN_POINT('Ctrl Pts',(7.46165237939775,3.1931078304343,-3.37307897121081));
#58874=CARTESIAN_POINT('',(7.49999999999943,3.2496519225041,-3.25572762720846));
#58875=CARTESIAN_POINT('Ctrl Pts',(7.49999999999096,3.25205165383167,-3.25205165383206));
#58876=CARTESIAN_POINT('Ctrl Pts',(7.49999999570083,3.25125200145742,-3.25327719982305));
#58877=CARTESIAN_POINT('Ctrl Pts',(7.50000000037144,3.25045209686877,-3.25450251208352));
#58878=CARTESIAN_POINT('Ctrl Pts',(7.50000000105118,3.24965192115593,-3.25572762689991));
#58879=CARTESIAN_POINT('Ctrl Pts',(7.50000000105064,3.24965192115513,-3.2557276269016));
#58880=CARTESIAN_POINT('Ctrl Pts',(7.48748585582718,3.23096570291725,-3.29500700498933));
#58881=CARTESIAN_POINT('Ctrl Pts',(7.47470152024076,3.21211511774079,-3.33412233455541));
#58882=CARTESIAN_POINT('Ctrl Pts',(7.46165237939775,3.1931078304343,-3.37307897121081));
#58883=CARTESIAN_POINT('Ctrl Pts',(7.21281435372989,4.58165253645099,-1.09642934688623));
#58884=CARTESIAN_POINT('Ctrl Pts',(7.19993346366796,4.58523137267456,-1.14112866266571));
#58885=CARTESIAN_POINT('Ctrl Pts',(7.18694338462305,4.58871947646029,-1.18580378192547));
#58886=CARTESIAN_POINT('Ctrl Pts',(7.17384635845203,4.59212072600842,-1.23045504008016));
#58887=CARTESIAN_POINT('Ctrl Pts',(7.30892798333139,4.53504334164142,-1.1278566518479));
#58888=CARTESIAN_POINT('Ctrl Pts',(7.29604661499953,4.53862178188794,-1.17255586152563));
#58889=CARTESIAN_POINT('Ctrl Pts',(7.28299669995025,4.54206016538018,-1.21721772087862));
#58890=CARTESIAN_POINT('Ctrl Pts',(7.26978169876727,4.54536447860045,-1.26184274766094));
#58891=CARTESIAN_POINT('Ctrl Pts',(7.40504161293289,4.48843414683185,-1.15928395680956));
#58892=CARTESIAN_POINT('Ctrl Pts',(7.39215976633109,4.49201219110133,-1.20398306038554));
#58893=CARTESIAN_POINT('Ctrl Pts',(7.37905001527745,4.49540085430006,-1.24863165983177));
#58894=CARTESIAN_POINT('Ctrl Pts',(7.36571703908251,4.49860823119249,-1.29323045524171));
#58895=CARTESIAN_POINT('Ctrl Pts',(7.50115524253438,4.44182495202228,-1.19071126177122));
#58896=CARTESIAN_POINT('Ctrl Pts',(7.48827291766266,4.44540260031471,-1.23541025924545));
#58897=CARTESIAN_POINT('Ctrl Pts',(7.47510333060465,4.44874154321995,-1.28004559878492));
#58898=CARTESIAN_POINT('Ctrl Pts',(7.46165237939775,4.45185198378452,-1.32461816282249));
#58899=CARTESIAN_POINT('',(7.49999999999943,4.44214493194972,-1.19471687171331));
#58900=CARTESIAN_POINT('Ctrl Pts',(7.49999999999096,4.44238517355345,-1.19033351972193));
#58901=CARTESIAN_POINT('Ctrl Pts',(7.49999999569755,4.44230542728599,-1.19179469976444));
#58902=CARTESIAN_POINT('Ctrl Pts',(7.50000000037144,4.44222534572098,-1.1932558035927));
#58903=CARTESIAN_POINT('Ctrl Pts',(7.50000000105118,4.4421449306279,-1.19471687212018));
#58904=CARTESIAN_POINT('Ctrl Pts',(7.50000000105064,4.44214493062805,-1.19471687212205));
#58905=CARTESIAN_POINT('Ctrl Pts',(7.48748585582718,4.44560187997725,-1.23807692050981));
#58906=CARTESIAN_POINT('Ctrl Pts',(7.47470152024076,4.44883445912128,-1.28137708217967));
#58907=CARTESIAN_POINT('Ctrl Pts',(7.46165237939775,4.45185198378452,-1.32461816282249));
#58908=CARTESIAN_POINT('Origin',(1.5,-1.01951846029017E-15,-5.55));
#58909=CARTESIAN_POINT('',(1.6,2.49998034634996,-3.8267625540171));
#58910=CARTESIAN_POINT('Origin',(1.5,-2.775,-4.80644099100363));
#58911=CARTESIAN_POINT('',(1.6,0.558573497940197,-4.53948635285801));
#58912=CARTESIAN_POINT('Origin',(1.5,-4.80644099100363,-2.775));
#58913=CARTESIAN_POINT('',(1.6,-1.93611308191135,-4.13925137399521));
#58914=CARTESIAN_POINT('Origin',(1.5,-5.55,6.79678973526781E-16));
#58915=CARTESIAN_POINT('',(1.6,-4.08446337701807,-2.12612183123792));
#58916=CARTESIAN_POINT('Origin',(7.5,0.,0.));
#58917=CARTESIAN_POINT('Origin',(7.5,0.,0.));
#58918=CARTESIAN_POINT('Origin',(7.5,0.,0.));
#58919=CARTESIAN_POINT('Origin',(7.5,0.,0.));
#58920=CARTESIAN_POINT('Origin',(7.5,0.,0.));
#58921=CARTESIAN_POINT('Origin',(7.5,0.,0.));
#58922=CARTESIAN_POINT('Origin',(7.5,0.,0.));
#58923=CARTESIAN_POINT('Origin',(7.5,0.,0.));
#58924=CARTESIAN_POINT('Origin',(7.5,0.,0.));
#58925=CARTESIAN_POINT('',(7.5,-3.95,4.83735485663205E-16));
#58926=CARTESIAN_POINT('Origin',(7.5,0.,0.));
#58927=CARTESIAN_POINT('Origin',(6.9,0.,0.));
#58928=CARTESIAN_POINT('Origin',(6.9,0.,0.));
#58929=CARTESIAN_POINT('Origin',(6.9,0.,0.));
#58930=CARTESIAN_POINT('Origin',(6.9,0.,0.));
#58931=CARTESIAN_POINT('Origin',(6.9,0.,0.));
#58932=CARTESIAN_POINT('Origin',(6.9,0.,0.));
#58933=CARTESIAN_POINT('Origin',(6.9,0.,0.));
#58934=CARTESIAN_POINT('Origin',(6.9,0.,0.));
#58935=CARTESIAN_POINT('Origin',(7.35,0.,0.));
#58936=CARTESIAN_POINT('',(7.1,-3.55,-4.3474961369731E-16));
#58937=CARTESIAN_POINT('Origin',(7.1,0.,0.));
#58938=CARTESIAN_POINT('',(7.35,-3.8,-4.65365783675994E-16));
#58939=CARTESIAN_POINT('Origin',(0.15,0.,0.));
#58940=CARTESIAN_POINT('',(0.,-3.95,-4.83735485663205E-16));
#58941=CARTESIAN_POINT('Origin',(0.,0.,0.));
#58942=CARTESIAN_POINT('',(0.400000000000001,-3.55,-4.3474961369731E-16));
#58943=CARTESIAN_POINT('',(0.15,-3.8,-4.65365783675994E-16));
#58944=CARTESIAN_POINT('Origin',(0.4,0.,0.));
#58945=CARTESIAN_POINT('Origin',(1.5,4.80644099100363,-2.775));
#58946=CARTESIAN_POINT('',(1.6,4.69203409014831,-1.34635348791082));
#58947=CARTESIAN_POINT('Origin',(1.5,2.775,-4.80644099100363));
#58948=CARTESIAN_POINT('',(1.6,3.77815762639755,-2.69583924476141));
#58949=CARTESIAN_POINT('Origin',(1.5,-4.80644099100363,2.775));
#58950=CARTESIAN_POINT('',(1.6,-4.66941333870903,1.06387876476949));
#58951=CARTESIAN_POINT('Origin',(1.5,-2.775,4.80644099100363));
#58952=CARTESIAN_POINT('',(1.6,-3.12397753684527,4.07220682950901));
#58953=CARTESIAN_POINT('Origin',(1.5,3.3983948676339E-16,5.55));
#58954=CARTESIAN_POINT('',(1.6,-0.0934210082369602,5.48560486190603));
#58955=CARTESIAN_POINT('Origin',(1.5,2.775,4.80644099100363));
#58956=CARTESIAN_POINT('',(1.6,2.96880575062052,4.82196107599933));
#58957=CARTESIAN_POINT('Origin',(1.5,4.80644099100363,2.775));
#58958=CARTESIAN_POINT('',(1.6,4.83193299235907,2.76288378924761));
#58959=CARTESIAN_POINT('Origin',(1.5,5.55,0.));
#58960=CARTESIAN_POINT('',(1.6,5.22790403890507,0.467279523348994));
#58961=CARTESIAN_POINT('Origin',(0.8,0.,0.));
#58962=CARTESIAN_POINT('',(0.8,-3.55,-4.3474961369731E-16));
#58963=CARTESIAN_POINT('Origin',(0.,6.2,0.));
#58964=CARTESIAN_POINT('',(-3.46944695195361E-17,-6.2,-7.59281015471359E-16));
#58965=CARTESIAN_POINT('Origin',(0.,0.,0.));
#58966=CARTESIAN_POINT('Origin',(0.15,0.,0.));
#58967=CARTESIAN_POINT('',(0.3,-6.5,-7.9602041944578E-16));
#58968=CARTESIAN_POINT('Origin',(0.3,0.,0.));
#58969=CARTESIAN_POINT('',(0.15,-6.35,-7.77650717458569E-16));
#58970=CARTESIAN_POINT('Origin',(0.85,0.,0.));
#58971=CARTESIAN_POINT('',(1.4,-6.5,-7.9602041944578E-16));
#58972=CARTESIAN_POINT('Origin',(1.4,0.,0.));
#58973=CARTESIAN_POINT('',(0.85,-6.5,-7.9602041944578E-16));
#58974=CARTESIAN_POINT('Origin',(1.5,0.,0.));
#58975=CARTESIAN_POINT('',(1.6,-6.,-7.34788079488412E-16));
#58976=CARTESIAN_POINT('Origin',(1.6,0.,0.));
#58977=CARTESIAN_POINT('',(1.5,-6.25,-7.65404249467096E-16));
#58978=CARTESIAN_POINT('Origin',(1.6,3.55,0.));
#60350=UNCERTAINTY_MEASURE_WITH_UNIT(LENGTH_MEASURE(0.01),#60366,
'DISTANCE_ACCURACY_VALUE',
'Maximum model space distance between geometric entities at asserted c
onnectivities');
#60353=UNCERTAINTY_MEASURE_WITH_UNIT(LENGTH_MEASURE(0.01),#60366,
'DISTANCE_ACCURACY_VALUE',
'Maximum model space distance between geometric entities at asserted c
onnectivities');
#60362=(
GEOMETRIC_REPRESENTATION_CONTEXT(3)
GLOBAL_UNCERTAINTY_ASSIGNED_CONTEXT((#60350))
GLOBAL_UNIT_ASSIGNED_CONTEXT((#60366,#60368,#60369))
REPRESENTATION_CONTEXT('','3D')
);
#60365=(
GEOMETRIC_REPRESENTATION_CONTEXT(3)
GLOBAL_UNCERTAINTY_ASSIGNED_CONTEXT((#60353))
GLOBAL_UNIT_ASSIGNED_CONTEXT((#60366,#60368,#60369))
REPRESENTATION_CONTEXT('','3D')
);
#60366=(
LENGTH_UNIT()
NAMED_UNIT(*)
SI_UNIT(.MILLI.,.METRE.)
);
#60368=(
NAMED_UNIT(*)
PLANE_ANGLE_UNIT()
SI_UNIT($,.RADIAN.)
);
#60369=(
NAMED_UNIT(*)
SI_UNIT($,.STERADIAN.)
SOLID_ANGLE_UNIT()
);
#60378=SHAPE_DEFINITION_REPRESENTATION(#60389,#60414);
#60389=PRODUCT_DEFINITION_SHAPE('',$,#60426);
#60414=SHAPE_REPRESENTATION('',(#19368),#60362);
#60417=PRODUCT_DEFINITION_CONTEXT('part definition',#60452,'design');
#60426=PRODUCT_DEFINITION('2026-10-25-00-06-43-044',
'10_Compressor_Locknut_12pt_M7x1_LH',#60437,#60417);
#60437=PRODUCT_DEFINITION_FORMATION('',$,#60462);
#60452=APPLICATION_CONTEXT(
'Core Data for Automotive Mechanical Design Process');
#60453=PRODUCT_CONTEXT('part definition',#60452,'mechanical');
#60462=PRODUCT('2026-10-25-00-06-43-044',
'10_Compressor_Locknut_12pt_M7x1_LH',$,(#60453));
#60528=COLOUR_RGB('Black',0.12,0.14,0.17);
#60529=FILL_AREA_STYLE_COLOUR('',#60528);
#60530=FILL_AREA_STYLE('',(#60529));
#60531=SURFACE_STYLE_FILL_AREA(#60530);
#60532=SURFACE_SIDE_STYLE('',(#60531));
#60533=SURFACE_STYLE_USAGE(.BOTH.,#60532);
#60534=PRESENTATION_STYLE_ASSIGNMENT((#60533));
ENDSEC;
END-ISO-10303-21;
